ISO-10303-21;
HEADER;
FILE_DESCRIPTION (('STEP AP214'),
    '1' );
FILE_NAME ('base.step',
    '2026-10-28T16:30:29',
    ( '' ),
    ( '' ),
    'SwSTEP 2.0',
    'SolidWorks 2025',
    '' );
FILE_SCHEMA (( 'AUTOMOTIVE_DESIGN' ));
ENDSEC;

DATA;
#2=AXIS2_PLACEMENT_3D ( 'NONE', #7401, #6721, #5569 ) ;
#3=VERTEX_POINT ( 'NONE', #4491 ) ;
#4=VECTOR ( 'NONE', #6644, 1000.000000000000000 ) ;
#5=ADVANCED_FACE ( 'NONE', ( #5063 ), #903, .F. ) ;
#11=AXIS2_PLACEMENT_3D ( 'NONE', #6403, #3479, #547 ) ;
#14=AXIS2_PLACEMENT_3D ( 'NONE', #4631, #3929, #1078 ) ;
#23=AXIS2_PLACEMENT_3D ( 'NONE', #5950, #680, #1328 ) ;
#24=ORIENTED_EDGE ( 'NONE', *, *, #3857, .T. ) ;
#26=CARTESIAN_POINT ( 'NONE',  ( 3.000000000000002665, 0.000000000000000000, 35.00000000000000000 ) ) ;
#27=LINE ( 'NONE', #5419, #4744 ) ;
#28=CARTESIAN_POINT ( 'NONE',  ( 188.6380400399839061, 9.000000000000001776, 15.00000000000000888 ) ) ;
#32=ORIENTED_EDGE ( 'NONE', *, *, #3252, .F. ) ;
#35=ORIENTED_EDGE ( 'NONE', *, *, #1878, .T. ) ;
#40=EDGE_CURVE ( 'NONE', #3862, #1645, #5779, .T. ) ;
#41=EDGE_LOOP ( 'NONE', ( #5508, #4352, #6797, #4752 ) ) ;
#43=AXIS2_PLACEMENT_3D ( 'NONE', #7599, #4696, #644 ) ;
#46=CARTESIAN_POINT ( 'NONE',  ( 209.9999999999999716, -3.000000000000000888, 35.00000000000000000 ) ) ;
#49=SHAPE_DEFINITION_REPRESENTATION ( #3722, #915 ) ;
#50=DIRECTION ( 'NONE',  ( -1.000000000000000000, -0.000000000000000000, -0.000000000000000000 ) ) ;
#52=AXIS2_PLACEMENT_3D ( 'NONE', #1456, #3815, #1490 ) ;
#54=EDGE_CURVE ( 'NONE', #3265, #5898, #5654, .T. ) ;
#55=ADVANCED_FACE ( 'NONE', ( #5029 ), #3220, .F. ) ;
#62=DIRECTION ( 'NONE',  ( 0.000000000000000000, 0.000000000000000000, 1.000000000000000000 ) ) ;
#64=CARTESIAN_POINT ( 'NONE',  ( 3.000000000000002665, 30.03170604878415162, 13.00000000000001066 ) ) ;
#66=VECTOR ( 'NONE', #761, 1000.000000000000000 ) ;
#72=DIRECTION ( 'NONE',  ( 0.000000000000000000, -0.03489949670250429292, -0.9993908270190956511 ) ) ;
#73=PLANE ( 'NONE',  #5716 ) ;
#77=CARTESIAN_POINT ( 'NONE',  ( 187.7594781219628999, -3.757281668791117468, 16.47828612039246465 ) ) ;
#80=EDGE_CURVE ( 'NONE', #4729, #1895, #4308, .T. ) ;
#82=CARTESIAN_POINT ( 'NONE',  ( 220.0000000000000000, -56.99999999999999289, 7.000000000000000888 ) ) ;
#83=ORIENTED_EDGE ( 'NONE', *, *, #275, .T. ) ;
#85=AXIS2_PLACEMENT_3D ( 'NONE', #4576, #2304, #5803 ) ;
#87=DIRECTION ( 'NONE',  ( 1.000000000000000000, 0.000000000000000000, 0.000000000000000000 ) ) ;
#88=ORIENTED_EDGE ( 'NONE', *, *, #483, .F. ) ;
#90=AXIS2_PLACEMENT_3D ( 'NONE', #1507, #1400, #825 ) ;
#98=CARTESIAN_POINT ( 'NONE',  ( 217.0000000000000000, 20.99999999999999645, 13.00000000000000888 ) ) ;
#99=AXIS2_PLACEMENT_3D ( 'NONE', #6628, #2937, #5286 ) ;
#103=EDGE_CURVE ( 'NONE', #1980, #3365, #5258, .T. ) ;
#107=CYLINDRICAL_SURFACE ( 'NONE', #7534, 3.000000000000000000 ) ;
#109=CARTESIAN_POINT ( 'NONE',  ( 190.0729179104125137, 6.000000000000001776, 16.24264068711929454 ) ) ;
#111=ADVANCED_FACE ( 'NONE', ( #6250 ), #4449, .F. ) ;
#117=ORIENTED_EDGE ( 'NONE', *, *, #841, .F. ) ;
#119=CARTESIAN_POINT ( 'NONE',  ( 217.0000000000000000, 56.99999999999999289, 2.149255132503604690E-14 ) ) ;
#124=EDGE_CURVE ( 'NONE', #3147, #3862, #1554, .T. ) ;
#126=( BOUNDED_SURFACE ( )  B_SPLINE_SURFACE ( 3, 2, ( 
 ( #6358, #1115, #535 ),
 ( #7576, #4667, #7000 ),
 ( #5776, #2923, #7425 ),
 ( #2158, #4511, #999 ),
 ( #424, #6970, #2887 ),
 ( #5124, #7466, #686 ),
 ( #2497, #3699, #5310 ),
 ( #4202, #3048, #6003 ),
 ( #6470, #4707, #3588 ),
 ( #1190, #4166, #614 ) ),
 .UNSPECIFIED., .F., .F., .F. ) 
 B_SPLINE_SURFACE_WITH_KNOTS ( ( 4, 2, 2, 2, 4 ),
 ( 3, 3 ),
 ( 1.570796326794896558, 1.963495408493620697, 2.356194490192344837, 2.748893571891068976, 3.141592653589793116 ),
 ( 0.000000000000000000, 1.000000000000000000 ),
 .UNSPECIFIED. ) 
 GEOMETRIC_REPRESENTATION_ITEM ( )  RATIONAL_B_SPLINE_SURFACE ( (
 ( 1.000000000000000000, 0.7071067811865473507, 1.000000000000000000),
 ( 1.000000000000000000, 0.7087223175983969892, 1.000000000000000000),
 ( 1.000000000000000000, 0.7103306498028938432, 1.000000000000000000),
 ( 1.000000000000000000, 0.7132953257861496255, 1.000000000000000000),
 ( 1.000000000000000000, 0.7146502351234478301, 1.000000000000000000),
 ( 1.000000000000000000, 0.7169067290091972744, 1.000000000000000000),
 ( 1.000000000000000000, 0.7178075805514493313, 1.000000000000000000),
 ( 1.000000000000000000, 0.7190243029327590962, 1.000000000000000000),
 ( 1.000000000000000000, 0.7193412045353504425, 1.000000000000000000),
 ( 1.000000000000000000, 0.7193398003386524131, 1.000000000000000000) ) ) 
 REPRESENTATION_ITEM ( '' )  SURFACE ( )  );
#129=CARTESIAN_POINT ( 'NONE',  ( 43.50000000000001421, 39.99999999999999289, 0.000000000000000000 ) ) ;
#131=VERTEX_POINT ( 'NONE', #5107 ) ;
#132=CARTESIAN_POINT ( 'NONE',  ( 47.00000000000000000, 0.000000000000000000, 35.00000000000000000 ) ) ;
#137=DIRECTION ( 'NONE',  ( 0.000000000000000000, -1.000000000000000000, 0.000000000000000000 ) ) ;
#139=SPHERICAL_SURFACE ( 'NONE', #1773, 3.000000000000000000 ) ;
#140=CARTESIAN_POINT ( 'NONE',  ( 26.49999999999999645, -39.99999999999999289, 0.000000000000000000 ) ) ;
#144=ORIENTED_EDGE ( 'NONE', *, *, #928, .F. ) ;
#147=DIRECTION ( 'NONE',  ( -0.000000000000000000, 1.000000000000000000, 1.836970198721029934E-16 ) ) ;
#151=VECTOR ( 'NONE', #2336, 1000.000000000000000 ) ;
#153=ORIENTED_EDGE ( 'NONE', *, *, #1028, .T. ) ;
#161=ORIENTED_EDGE ( 'NONE', *, *, #5968, .F. ) ;
#168=EDGE_LOOP ( 'NONE', ( #6133, #5211, #83, #575 ) ) ;
#170=FACE_BOUND ( 'NONE', #6243, .T. ) ;
#172=DIRECTION ( 'NONE',  ( 0.000000000000000000, 0.000000000000000000, 1.000000000000000000 ) ) ;
#174=DIRECTION ( 'NONE',  ( -0.000000000000000000, -0.000000000000000000, 1.000000000000000000 ) ) ;
#175=LINE ( 'NONE', #5523, #4427 ) ;
#176=AXIS2_PLACEMENT_3D ( 'NONE', #3789, #147, #6778 ) ;
#180=DIRECTION ( 'NONE',  ( 0.000000000000000000, 1.000000000000000000, 0.000000000000000000 ) ) ;
#189=AXIS2_PLACEMENT_3D ( 'NONE', #7070, #4732, #2989 ) ;
#194=CARTESIAN_POINT ( 'NONE',  ( 220.0000000000000000, -56.99999999999999289, 3.000000000000000444 ) ) ;
#197=EDGE_CURVE ( 'NONE', #2264, #3547, #4063, .T. ) ;
#202=EDGE_LOOP ( 'NONE', ( #4107, #646, #7588, #6121 ) ) ;
#204=APPLICATION_CONTEXT ( 'automotive_design' ) ;
#207=EDGE_CURVE ( 'NONE', #5755, #6501, #4651, .T. ) ;
#209=DIRECTION ( 'NONE',  ( 1.000000000000000000, 0.000000000000000000, 0.000000000000000000 ) ) ;
#211=ORIENTED_EDGE ( 'NONE', *, *, #5767, .T. ) ;
#217=CYLINDRICAL_SURFACE ( 'NONE', #3317, 2.999999999999999112 ) ;
#219=EDGE_CURVE ( 'NONE', #2614, #3744, #5836, .T. ) ;
#220=VECTOR ( 'NONE', #5591, 1000.000000000000000 ) ;
#221=CARTESIAN_POINT ( 'NONE',  ( 217.0000000000000000, 3.000000000000000888, 18.00000000000001066 ) ) ;
#225=EDGE_LOOP ( 'NONE', ( #3231, #2812 ) ) ;
#230=FACE_OUTER_BOUND ( 'NONE', #6873, .T. ) ;
#231=DIRECTION ( 'NONE',  ( 0.000000000000000000, 0.9993908270190956511, -0.03489949670250429986 ) ) ;
#233=VERTEX_POINT ( 'NONE', #7594 ) ;
#234=ADVANCED_FACE ( 'NONE', ( #2330 ), #7023, .F. ) ;
#239=CARTESIAN_POINT ( 'NONE',  ( 220.0000000000000000, -56.99999999999999289, 10.00000000000000000 ) ) ;
#240=CARTESIAN_POINT ( 'NONE',  ( 3.000000000000002665, -56.99999999999999289, 5.510910596163094486E-16 ) ) ;
#242=EDGE_CURVE ( 'NONE', #131, #233, #7369, .T. ) ;
#243=DIRECTION ( 'NONE',  ( 0.000000000000000000, -1.000000000000000000, -1.836970198721029934E-16 ) ) ;
#244=DIRECTION ( 'NONE',  ( 1.000000000000000000, 0.000000000000000000, 0.000000000000000000 ) ) ;
#246=DIRECTION ( 'NONE',  ( -0.000000000000000000, 1.000000000000000000, -0.000000000000000000 ) ) ;
#247=LINE ( 'NONE', #3324, #6888 ) ;
#252=CARTESIAN_POINT ( 'NONE',  ( 217.0000000000000000, 3.000000000000000000, 35.00000000000000000 ) ) ;
#256=ADVANCED_FACE ( 'NONE', ( #6670 ), #4293, .F. ) ;
#258=VERTEX_POINT ( 'NONE', #1288 ) ;
#260=VECTOR ( 'NONE', #2250, 1000.000000000000000 ) ;
#262=ORIENTED_EDGE ( 'NONE', *, *, #1741, .F. ) ;
#264=ADVANCED_FACE ( 'NONE', ( #4799 ), #3938, .T. ) ;
#265=CARTESIAN_POINT ( 'NONE',  ( 47.00000000000000000, 0.000000000000000000, 35.00000000000000000 ) ) ;
#267=CARTESIAN_POINT ( 'NONE',  ( 26.49999999999999645, 39.99999999999999289, 0.000000000000000000 ) ) ;
#271=EDGE_CURVE ( 'NONE', #459, #258, #2406, .T. ) ;
#275=EDGE_CURVE ( 'NONE', #2163, #5513, #3192, .T. ) ;
#276=CARTESIAN_POINT ( 'NONE',  ( 0.000000000000000000, -5.510910596163110263E-16, 3.000000000000011102 ) ) ;
#280=CARTESIAN_POINT ( 'NONE',  ( 47.00000000000000000, 27.04312195450891565, 12.73853277175702203 ) ) ;
#283=DIRECTION ( 'NONE',  ( 0.000000000000000000, -0.000000000000000000, 1.000000000000000000 ) ) ;
#285=DIRECTION ( 'NONE',  ( 0.4999999999999976130, 0.000000000000000000, 0.8660254037844399289 ) ) ;
#290=CIRCLE ( 'NONE', #2131, 2.999999999999999112 ) ;
#292=DIRECTION ( 'NONE',  ( -1.000000000000000000, -0.000000000000000000, -0.000000000000000000 ) ) ;
#294=CARTESIAN_POINT ( 'NONE',  ( 188.3757902719622450, -8.737358564324091859, 15.00000000000001066 ) ) ;
#295=DIRECTION ( 'NONE',  ( -0.000000000000000000, 1.000000000000000000, -0.000000000000000000 ) ) ;
#297=ORIENTED_EDGE ( 'NONE', *, *, #778, .T. ) ;
#299=CARTESIAN_POINT ( 'NONE',  ( 26.49999999999999645, 39.99999999999999289, 0.000000000000000000 ) ) ;
#300=AXIS2_PLACEMENT_3D ( 'NONE', #4781, #6581, #3079 ) ;
#301=CARTESIAN_POINT ( 'NONE',  ( 217.0000000000000000, -20.99999999999999645, 7.000000000000008882 ) ) ;
#305=ORIENTED_EDGE ( 'NONE', *, *, #103, .F. ) ;
#310=ORIENTED_EDGE ( 'NONE', *, *, #2775, .F. ) ;
#317=ADVANCED_FACE ( 'NONE', ( #4185 ), #5986, .T. ) ;
#319=CARTESIAN_POINT ( 'NONE',  ( 187.5739056480075533, 3.719611233821797036, 16.15686516701557807 ) ) ;
#326=ORIENTED_EDGE ( 'NONE', *, *, #2285, .T. ) ;
#327=EDGE_CURVE ( 'NONE', #5270, #4738, #3066, .T. ) ;
#334=AXIS2_PLACEMENT_3D ( 'NONE', #7079, #1650, #1144 ) ;
#335=ORIENTED_EDGE ( 'NONE', *, *, #3931, .F. ) ;
#342=ORIENTED_EDGE ( 'NONE', *, *, #7222, .F. ) ;
#343=CARTESIAN_POINT ( 'NONE',  ( 50.00000000000000000, -17.91234734164656928, 13.00000000000000888 ) ) ;
#348=ORIENTED_EDGE ( 'NONE', *, *, #6825, .T. ) ;
#351=ORIENTED_EDGE ( 'NONE', *, *, #1487, .T. ) ;
#354=CARTESIAN_POINT ( 'NONE',  ( 203.9378221735088914, 6.000000000000000000, 38.49999999999997868 ) ) ;
#355=CARTESIAN_POINT ( 'NONE',  ( 217.0000000000000000, 56.99999999999999289, 3.000000000000021316 ) ) ;
#358=CARTESIAN_POINT ( 'NONE',  ( 47.00000000000000000, 21.91628335801839356, 36.91742634044857141 ) ) ;
#360=FACE_OUTER_BOUND ( 'NONE', #1701, .T. ) ;
#367=ADVANCED_FACE ( 'NONE', ( #3099 ), #3945, .T. ) ;
#371=ORIENTED_EDGE ( 'NONE', *, *, #1452, .T. ) ;
#375=CARTESIAN_POINT ( 'NONE',  ( 43.50000000000001421, -39.99999999999999289, 0.000000000000000000 ) ) ;
#381=VECTOR ( 'NONE', #2727, 1000.000000000000000 ) ;
#383=CARTESIAN_POINT ( 'NONE',  ( 220.0000000000000000, 9.000000000000001776, 12.00000000000000711 ) ) ;
#392=AXIS2_PLACEMENT_3D ( 'NONE', #5521, #246, #4948 ) ;
#394=LINE ( 'NONE', #3907, #3581 ) ;
#395=DIRECTION ( 'NONE',  ( 1.000000000000000000, 0.000000000000000000, 0.000000000000000000 ) ) ;
#396=ORIENTED_EDGE ( 'NONE', *, *, #40, .T. ) ;
#398=ADVANCED_FACE ( 'NONE', ( #5094 ), #5522, .F. ) ;
#399=PLANE ( 'NONE',  #3904 ) ;
#400=CARTESIAN_POINT ( 'NONE',  ( 190.3479161152068286, 6.383114783474912457, 16.48079611847125392 ) ) ;
#404=CARTESIAN_POINT ( 'NONE',  ( 53.00000000000002132, 60.00000000000000000, 10.00000000000002309 ) ) ;
#406=EDGE_CURVE ( 'NONE', #5445, #6726, #3208, .T. ) ;
#407=EDGE_LOOP ( 'NONE', ( #5425, #6759, #1885, #3552 ) ) ;
#408=DIRECTION ( 'NONE',  ( 1.000000000000000000, 0.000000000000000000, 0.000000000000000000 ) ) ;
#409=CYLINDRICAL_SURFACE ( 'NONE', #3526, 2.999999999999999112 ) ;
#412=FACE_OUTER_BOUND ( 'NONE', #6747, .T. ) ;
#415=EDGE_LOOP ( 'NONE', ( #4669, #5784, #1959, #6893 ) ) ;
#416=ORIENTED_EDGE ( 'NONE', *, *, #5323, .T. ) ;
#418=MECHANICAL_DESIGN_GEOMETRIC_PRESENTATION_REPRESENTATION('',(#786),#5839);
#422=LINE ( 'NONE', #383, #2018 ) ;
#423=ORIENTED_EDGE ( 'NONE', *, *, #430, .F. ) ;
#424=CARTESIAN_POINT ( 'NONE',  ( 51.79800105182081182, -26.47119478651012514, 10.00000000000000533 ) ) ;
#425=CARTESIAN_POINT ( 'NONE',  ( 51.46767767233086488, -19.46767767233084712, 10.00000000000001066 ) ) ;
#426=CIRCLE ( 'NONE', #7052, 3.000000000000004885 ) ;
#427=AXIS2_PLACEMENT_3D ( 'NONE', #4064, #2862, #1091 ) ;
#428=AXIS2_PLACEMENT_3D ( 'NONE', #4264, #6030, #4882 ) ;
#429=VERTEX_POINT ( 'NONE', #5560 ) ;
#430=EDGE_CURVE ( 'NONE', #6206, #797, #247, .T. ) ;
#431=AXIS2_PLACEMENT_3D ( 'NONE', #4321, #1460, #846 ) ;
#437=DIRECTION ( 'NONE',  ( 0.000000000000000000, 0.03489949670250403618, 0.9993908270190956511 ) ) ;
#438=LINE ( 'NONE', #1161, #260 ) ;
#444=AXIS2_PLACEMENT_3D ( 'NONE', #3267, #7341, #2187 ) ;
#445=CARTESIAN_POINT ( 'NONE',  ( 188.6338938035227102, 8.633158558239344416, 14.99640925390055557 ) ) ;
#447=CARTESIAN_POINT ( 'NONE',  ( 35.00000000000000000, -39.99999999999999289, 0.000000000000000000 ) ) ;
#451=ORIENTED_EDGE ( 'NONE', *, *, #1471, .T. ) ;
#459=VERTEX_POINT ( 'NONE', #7439 ) ;
#460=FACE_BOUND ( 'NONE', #2532, .T. ) ;
#463=LINE ( 'NONE', #5158, #995 ) ;
#464=FACE_OUTER_BOUND ( 'NONE', #1341, .T. ) ;
#467=DIRECTION ( 'NONE',  ( 0.000000000000000000, 0.000000000000000000, -1.000000000000000000 ) ) ;
#470=CARTESIAN_POINT ( 'NONE',  ( 217.0000000000000000, 60.00000000000000000, 3.000000000000021760 ) ) ;
#471=DIRECTION ( 'NONE',  ( 0.8660254037844404840, 0.000000000000000000, -0.4999999999999968359 ) ) ;
#474=ORIENTED_EDGE ( 'NONE', *, *, #3322, .T. ) ;
#476=CARTESIAN_POINT ( 'NONE',  ( 47.00000000000000000, -28.78532416918554304, 10.00000000000000711 ) ) ;
#477=CARTESIAN_POINT ( 'NONE',  ( 192.1021416551216419, 6.000000000000000888, 18.00000000000001066 ) ) ;
#482=ORIENTED_EDGE ( 'NONE', *, *, #4932, .F. ) ;
#483=EDGE_CURVE ( 'NONE', #4729, #5898, #394, .T. ) ;
#484=CARTESIAN_POINT ( 'NONE',  ( 217.0000000000000000, 56.99999999999999289, 3.000000000000021760 ) ) ;
#485=DIRECTION ( 'NONE',  ( 0.000000000000000000, 0.000000000000000000, -1.000000000000000000 ) ) ;
#487=CARTESIAN_POINT ( 'NONE',  ( 50.04196010845020481, -18.04196010845019060, 12.50000000000000533 ) ) ;
#492=EDGE_CURVE ( 'NONE', #6160, #5563, #3866, .T. ) ;
#493=VECTOR ( 'NONE', #6241, 1000.000000000000000 ) ;
#494=SPHERICAL_SURFACE ( 'NONE', #5750, 3.000000000000000000 ) ;
#495=CARTESIAN_POINT ( 'NONE',  ( 209.9999999999999716, 6.000000000000000000, 35.00000000000000000 ) ) ;
#496=VERTEX_POINT ( 'NONE', #3251 ) ;
#497=DIRECTION ( 'NONE',  ( 0.000000000000000000, 0.000000000000000000, -1.000000000000000000 ) ) ;
#498=FACE_OUTER_BOUND ( 'NONE', #6861, .T. ) ;
#499=CIRCLE ( 'NONE', #2964, 3.000000000000000888 ) ;
#500=ORIENTED_EDGE ( 'NONE', *, *, #6435, .T. ) ;
#501=EDGE_LOOP ( 'NONE', ( #4994, #7270, #5403, #348 ) ) ;
#507=DIRECTION ( 'NONE',  ( 0.000000000000000000, -2.065146995210485681E-16, 1.000000000000000000 ) ) ;
#510=VERTEX_POINT ( 'NONE', #969 ) ;
#516=CARTESIAN_POINT ( 'NONE',  ( 188.7208530678142040, 8.237612771022048364, 15.07171818587141487 ) ) ;
#519=DIRECTION ( 'NONE',  ( -0.4999999999999976685, 0.000000000000000000, -0.8660254037844400399 ) ) ;
#524=FACE_OUTER_BOUND ( 'NONE', #2293, .T. ) ;
#525=DIRECTION ( 'NONE',  ( 1.000000000000000000, 0.000000000000000000, 0.000000000000000000 ) ) ;
#528=CIRCLE ( 'NONE', #4838, 8.500000000000007105 ) ;
#529=VERTEX_POINT ( 'NONE', #5054 ) ;
#530=ORIENTED_EDGE ( 'NONE', *, *, #778, .F. ) ;
#532=CARTESIAN_POINT ( 'NONE',  ( 220.0000000000000000, -20.99999999999999645, 7.000000000000007994 ) ) ;
#533=AXIS2_PLACEMENT_3D ( 'NONE', #1064, #5764, #3460 ) ;
#535=CARTESIAN_POINT ( 'NONE',  ( 49.99999999999999289, -22.78166690339260825, 13.00000000000000888 ) ) ;
#536=CARTESIAN_POINT ( 'NONE',  ( 3.000000000000000000, 56.99999999999999289, 3.000000000000021760 ) ) ;
#537=ADVANCED_FACE ( 'NONE', ( #2015 ), #2125, .F. ) ;
#538=ORIENTED_EDGE ( 'NONE', *, *, #2032, .F. ) ;
#541=EDGE_LOOP ( 'NONE', ( #1499, #3109, #161 ) ) ;
#544=ORIENTED_EDGE ( 'NONE', *, *, #6289, .T. ) ;
#547=DIRECTION ( 'NONE',  ( 0.000000000000000000, 0.000000000000000000, 1.000000000000000000 ) ) ;
#549=CARTESIAN_POINT ( 'NONE',  ( 53.00000000000000711, 7.269317423140909676E-15, 13.00000000000000178 ) ) ;
#550=ADVANCED_FACE ( 'NONE', ( #3363 ), #1049, .T. ) ;
#558=CARTESIAN_POINT ( 'NONE',  ( 217.0000000000000000, -60.00000000000000000, 10.00000000000000000 ) ) ;
#563=ORIENTED_EDGE ( 'NONE', *, *, #3101, .T. ) ;
#564=CARTESIAN_POINT ( 'NONE',  ( 50.00000000000000000, -15.08392021690038298, 15.00000000000000888 ) ) ;
#565=CARTESIAN_POINT ( 'NONE',  ( 203.9378221735088630, -3.000000000000000000, 38.50000000000000000 ) ) ;
#566=CARTESIAN_POINT ( 'NONE',  ( 190.3575543333202518, -6.378640834395509884, 16.48914306019513276 ) ) ;
#567=AXIS2_PLACEMENT_3D ( 'NONE', #26, #2835, #485 ) ;
#568=ADVANCED_FACE ( 'NONE', ( #2359 ), #5708, .T. ) ;
#570=VERTEX_POINT ( 'NONE', #4716 ) ;
#571=EDGE_CURVE ( 'NONE', #7349, #2238, #438, .T. ) ;
#574=DIRECTION ( 'NONE',  ( 0.000000000000000000, 0.000000000000000000, -1.000000000000000000 ) ) ;
#575=ORIENTED_EDGE ( 'NONE', *, *, #667, .F. ) ;
#576=CARTESIAN_POINT ( 'NONE',  ( 190.0729179104125137, -6.000000000000001776, 16.24264068711929454 ) ) ;
#577=DIRECTION ( 'NONE',  ( -0.000000000000000000, -0.000000000000000000, 1.000000000000000000 ) ) ;
#579=AXIS2_PLACEMENT_3D ( 'NONE', #7169, #4831, #3601 ) ;
#584=VERTEX_POINT ( 'NONE', #7547 ) ;
#585=EDGE_CURVE ( 'NONE', #1652, #3936, #2782, .T. ) ;
#587=DIRECTION ( 'NONE',  ( 1.000000000000000000, 0.000000000000000000, 0.000000000000000000 ) ) ;
#588=CARTESIAN_POINT ( 'NONE',  ( 3.000000000000000000, -56.99999999999999289, 3.000000000000000444 ) ) ;
#593=DIRECTION ( 'NONE',  ( -0.000000000000000000, 1.000000000000000000, 2.065146995210484941E-16 ) ) ;
#597=VERTEX_POINT ( 'NONE', #470 ) ;
#601=DIRECTION ( 'NONE',  ( 0.000000000000000000, 0.000000000000000000, -1.000000000000000000 ) ) ;
#602=CARTESIAN_POINT ( 'NONE',  ( 186.9464254547409041, 5.771749062884673265, 15.00000000000001066 ) ) ;
#603=EDGE_CURVE ( 'NONE', #1345, #3492, #624, .T. ) ;
#604=CARTESIAN_POINT ( 'NONE',  ( 189.0505338480733428, -3.000000000000787814, 18.71446023341851372 ) ) ;
#606=ORIENTED_EDGE ( 'NONE', *, *, #54, .F. ) ;
#610=ADVANCED_FACE ( 'NONE', ( #1619 ), #6368, .T. ) ;
#612=VECTOR ( 'NONE', #2712, 1000.000000000000000 ) ;
#614=CARTESIAN_POINT ( 'NONE',  ( 46.99999999999999289, -25.78715168812825453, 12.89530150989249258 ) ) ;
#617=ORIENTED_EDGE ( 'NONE', *, *, #6748, .T. ) ;
#618=VECTOR ( 'NONE', #4221, 1000.000000000000000 ) ;
#624=CIRCLE ( 'NONE', #1472, 13.99999999999999112 ) ;
#625=DIRECTION ( 'NONE',  ( 0.000000000000000000, 0.000000000000000000, -1.000000000000000000 ) ) ;
#626=( BOUNDED_CURVE ( )  B_SPLINE_CURVE ( 3, ( #3067, #2370, #1289, #3648 ),
 .UNSPECIFIED., .F., .T. ) 
 B_SPLINE_CURVE_WITH_KNOTS ( ( 4, 4 ),
 ( 3.309040732809481966, 4.712388980384687898 ),
 .UNSPECIFIED. ) 
 CURVE ( )  GEOMETRIC_REPRESENTATION_ITEM ( )  RATIONAL_B_SPLINE_CURVE ( ( 1.000000000000000000, 0.8425084105506491783, 0.8425084105506491783, 1.000000000000000000 ) ) 
 REPRESENTATION_ITEM ( '' )  );
#632=( LENGTH_UNIT ( ) NAMED_UNIT ( * ) SI_UNIT ( .MILLI., .METRE. ) );
#634=CARTESIAN_POINT ( 'NONE',  ( 53.00000000000000711, -22.78166690339260825, 13.00000000000000888 ) ) ;
#635=CYLINDRICAL_SURFACE ( 'NONE', #1469, 3.000000000000002665 ) ;
#641=DIRECTION ( 'NONE',  ( 0.000000000000000000, -1.000000000000000000, -3.304235192336776498E-16 ) ) ;
#644=DIRECTION ( 'NONE',  ( 0.000000000000000000, 0.000000000000000000, 1.000000000000000000 ) ) ;
#646=ORIENTED_EDGE ( 'NONE', *, *, #585, .F. ) ;
#647=VERTEX_POINT ( 'NONE', #5824 ) ;
#649=FACE_OUTER_BOUND ( 'NONE', #2456, .T. ) ;
#650=EDGE_LOOP ( 'NONE', ( #2954, #2166, #606, #1222 ) ) ;
#653=DIRECTION ( 'NONE',  ( -1.000000000000000000, 0.000000000000000000, 0.000000000000000000 ) ) ;
#654=EDGE_LOOP ( 'NONE', ( #88, #4351, #3432, #5827 ) ) ;
#656=EDGE_CURVE ( 'NONE', #7224, #7378, #6272, .T. ) ;
#657=ORIENTED_EDGE ( 'NONE', *, *, #971, .T. ) ;
#658=VECTOR ( 'NONE', #2207, 1000.000000000000000 ) ;
#660=DIRECTION ( 'NONE',  ( 0.000000000000000000, 0.000000000000000000, -1.000000000000000000 ) ) ;
#662=ORIENTED_EDGE ( 'NONE', *, *, #7419, .T. ) ;
#663=DIRECTION ( 'NONE',  ( -1.000000000000000000, -0.000000000000000000, -0.000000000000000000 ) ) ;
#667=EDGE_CURVE ( 'NONE', #5033, #5513, #2899, .T. ) ;
#671=AXIS2_PLACEMENT_3D ( 'NONE', #3826, #6742, #6159 ) ;
#672=( BOUNDED_SURFACE ( )  B_SPLINE_SURFACE ( 3, 2, ( 
 ( #5769, #2839, #5191 ),
 ( #7528, #2269, #4622 ),
 ( #1686, #7146, #6573 ),
 ( #5996, #3657, #720 ),
 ( #4734, #2488, #4845 ),
 ( #7181, #1915, #2914 ),
 ( #566, #5269, #77 ),
 ( #4266, #5879, #1298 ),
 ( #3614, #3074, #604 ),
 ( #5729, #4158, #5421 ) ),
 .UNSPECIFIED., .F., .F., .F. ) 
 B_SPLINE_SURFACE_WITH_KNOTS ( ( 4, 2, 2, 2, 4 ),
 ( 3, 3 ),
 ( 0.000000000000000000, 0.3926990816987241395, 0.7853981633974482790, 1.178097245096172418, 1.570796326794896558 ),
 ( 0.000000000000000000, 1.000000000000000000 ),
 .UNSPECIFIED. ) 
 GEOMETRIC_REPRESENTATION_ITEM ( )  RATIONAL_B_SPLINE_SURFACE ( (
 ( 1.000000000000000000, 0.8660254037844387076, 1.000000000000000000),
 ( 1.000000000000000000, 0.8660344512784944326, 1.000000000000000000),
 ( 1.000000000000000000, 0.8622916024758332521, 1.000000000000000000),
 ( 1.000000000000000000, 0.8476439321310361708, 1.000000000000000000),
 ( 1.000000000000000000, 0.8367284556825863584, 1.000000000000000000),
 ( 1.000000000000000000, 0.8086003203334847234, 1.000000000000000000),
 ( 1.000000000000000000, 0.7913838405144675292, 1.000000000000000000),
 ( 1.000000000000000000, 0.7522104819566599598, 1.000000000000000000),
 ( 1.000000000000000000, 0.7302616374798159837, 1.000000000000000000),
 ( 1.000000000000000000, 0.7071067811865475727, 1.000000000000000000) ) ) 
 REPRESENTATION_ITEM ( '' )  SURFACE ( )  );
#673=CARTESIAN_POINT ( 'NONE',  ( 176.5000000000000000, -39.99999999999999289, 0.000000000000000000 ) ) ;
#676=CARTESIAN_POINT ( 'NONE',  ( 217.0000000000000000, -3.000000000000000000, 0.000000000000000000 ) ) ;
#678=AXIS2_PLACEMENT_3D ( 'NONE', #4156, #3034, #3496 ) ;
#680=DIRECTION ( 'NONE',  ( 0.000000000000000000, -0.000000000000000000, 1.000000000000000000 ) ) ;
#682=EDGE_CURVE ( 'NONE', #797, #570, #859, .T. ) ;
#684=CARTESIAN_POINT ( 'NONE',  ( 35.00000000000000000, -39.99999999999999289, 0.000000000000000000 ) ) ;
#686=CARTESIAN_POINT ( 'NONE',  ( 48.84364016120891705, -25.18505342979141304, 12.91627608905694302 ) ) ;
#703=DIRECTION ( 'NONE',  ( -0.000000000000000000, -1.000000000000000000, -0.000000000000000000 ) ) ;
#710=ADVANCED_FACE ( 'NONE', ( #1346 ), #771, .F. ) ;
#711=DIRECTION ( 'NONE',  ( 1.000000000000000000, 0.000000000000000000, 0.000000000000000000 ) ) ;
#712=DIRECTION ( 'NONE',  ( 0.000000000000000000, 0.000000000000000000, -1.000000000000000000 ) ) ;
#713=EDGE_CURVE ( 'NONE', #5693, #4091, #1602, .T. ) ;
#714=LINE ( 'NONE', #5337, #939 ) ;
#720=CARTESIAN_POINT ( 'NONE',  ( 186.4771806038177147, -5.978286120977721829, 14.25728166854551660 ) ) ;
#722=VERTEX_POINT ( 'NONE', #4827 ) ;
#727=DIRECTION ( 'NONE',  ( 0.000000000000000000, 0.000000000000000000, 1.000000000000000000 ) ) ;
#729=ADVANCED_FACE ( 'NONE', ( #2549 ), #3016, .T. ) ;
#734=VERTEX_POINT ( 'NONE', #5366 ) ;
#735=DIRECTION ( 'NONE',  ( 1.000000000000000000, 0.000000000000000000, 0.000000000000000000 ) ) ;
#739=ORIENTED_EDGE ( 'NONE', *, *, #5880, .T. ) ;
#742=DIRECTION ( 'NONE',  ( -1.000000000000000000, -0.000000000000000000, -0.000000000000000000 ) ) ;
#744=CARTESIAN_POINT ( 'NONE',  ( 220.0000000000000000, 56.99999999999999289, 3.000000000000021760 ) ) ;
#746=ORIENTED_EDGE ( 'NONE', *, *, #831, .F. ) ;
#747=ADVANCED_FACE ( 'NONE', ( #4175 ), #2436, .F. ) ;
#750=CARTESIAN_POINT ( 'NONE',  ( 35.00000000000000000, -39.99999999999999289, 10.00000000000000355 ) ) ;
#751=DIRECTION ( 'NONE',  ( 0.000000000000000000, 0.9993908270190955401, -0.03489949670250403618 ) ) ;
#754=LINE ( 'NONE', #3182, #2092 ) ;
#756=EDGE_CURVE ( 'NONE', #5055, #4559, #2470, .T. ) ;
#758=ORIENTED_EDGE ( 'NONE', *, *, #2956, .T. ) ;
#761=DIRECTION ( 'NONE',  ( -0.000000000000000000, 1.000000000000000000, 2.065146995210484941E-16 ) ) ;
#764=DIRECTION ( 'NONE',  ( 0.000000000000000000, 0.000000000000000000, -1.000000000000000000 ) ) ;
#767=CARTESIAN_POINT ( 'NONE',  ( 50.00000000000000000, 0.000000000000000000, 35.00000000000000000 ) ) ;
#770=ADVANCED_FACE ( 'NONE', ( #7163, #4901 ), #5439, .T. ) ;
#771=CYLINDRICAL_SURFACE ( 'NONE', #6523, 8.500000000000007105 ) ;
#773=CARTESIAN_POINT ( 'NONE',  ( 209.9999999999999716, 6.000000000000000000, 35.00000000000000000 ) ) ;
#778=EDGE_CURVE ( 'NONE', #4559, #722, #1243, .T. ) ;
#779=CYLINDRICAL_SURFACE ( 'NONE', #4332, 3.000000000000000444 ) ;
#780=CIRCLE ( 'NONE', #6074, 6.000000000000000000 ) ;
#781=CARTESIAN_POINT ( 'NONE',  ( 35.00000000000000000, 39.99999999999999289, 10.00000000000000355 ) ) ;
#782=DIRECTION ( 'NONE',  ( 0.000000000000000000, -1.000000000000000000, 0.000000000000000000 ) ) ;
#785=VECTOR ( 'NONE', #6158, 1000.000000000000000 ) ;
#786=STYLED_ITEM('',(#7617),#6351);
#788=CARTESIAN_POINT ( 'NONE',  ( 220.0000000000000000, 9.000000000000001776, 12.00000000000000888 ) ) ;
#791=DIRECTION ( 'NONE',  ( -0.4999999999999967804, 0.000000000000000000, -0.8660254037844405950 ) ) ;
#795=ADVANCED_FACE ( 'NONE', ( #2508 ), #2973, .F. ) ;
#796=AXIS2_PLACEMENT_3D ( 'NONE', #6678, #5607, #2529 ) ;
#797=VERTEX_POINT ( 'NONE', #1821 ) ;
#801=CARTESIAN_POINT ( 'NONE',  ( 26.49999999999999645, 39.99999999999999289, 10.00000000000000355 ) ) ;
#803=LINE ( 'NONE', #2572, #1679 ) ;
#812=DIRECTION ( 'NONE',  ( 1.000000000000000000, 0.000000000000000000, 0.000000000000000000 ) ) ;
#813=EDGE_LOOP ( 'NONE', ( #2631, #3039, #4537, #1805, #3309 ) ) ;
#816=PLANE ( 'NONE',  #1687 ) ;
#817=DIRECTION ( 'NONE',  ( 0.000000000000000000, 0.000000000000000000, -1.000000000000000000 ) ) ;
#821=CARTESIAN_POINT ( 'NONE',  ( 3.000000000000002665, 56.99999999999999289, 7.000000000000022204 ) ) ;
#825=DIRECTION ( 'NONE',  ( 0.000000000000000000, -0.9993908270190955401, 0.03489949670250346025 ) ) ;
#830=EDGE_LOOP ( 'NONE', ( #7242, #2031, #1689, #6360 ) ) ;
#831=EDGE_CURVE ( 'NONE', #3147, #7378, #499, .T. ) ;
#834=DIRECTION ( 'NONE',  ( -1.000000000000000000, 0.000000000000000000, 0.000000000000000000 ) ) ;
#835=LINE ( 'NONE', #5536, #66 ) ;
#836=CARTESIAN_POINT ( 'NONE',  ( 50.00000000000000000, -25.88825784476432545, 10.00000000000001066 ) ) ;
#840=ADVANCED_FACE ( 'NONE', ( #7275 ), #6537, .T. ) ;
#841=EDGE_CURVE ( 'NONE', #2502, #6942, #5585, .T. ) ;
#843=CARTESIAN_POINT ( 'NONE',  ( 0.000000000000000000, 56.99999999999999289, 0.000000000000000000 ) ) ;
#845=DIRECTION ( 'NONE',  ( -2.775557561562885829E-15, 0.000000000000000000, -1.000000000000000000 ) ) ;
#846=DIRECTION ( 'NONE',  ( -1.000000000000000000, 0.000000000000000000, 0.000000000000000000 ) ) ;
#847=ORIENTED_EDGE ( 'NONE', *, *, #4444, .T. ) ;
#849=CARTESIAN_POINT ( 'NONE',  ( 48.57048730951211724, 29.87494558651862420, 10.00000000000000888 ) ) ;
#854=DIRECTION ( 'NONE',  ( -0.000000000000000000, 1.000000000000000000, 2.065146995210484941E-16 ) ) ;
#859=CIRCLE ( 'NONE', #6034, 2.999999999999999112 ) ;
#863=CARTESIAN_POINT ( 'NONE',  ( 3.000000000000002665, 56.99999999999999289, 7.000000000000021316 ) ) ;
#865=EDGE_CURVE ( 'NONE', #3936, #6541, #2469, .T. ) ;
#866=CIRCLE ( 'NONE', #4077, 3.000000000000000888 ) ;
#881=DIRECTION ( 'NONE',  ( 0.000000000000000000, 0.9860132971832693549, 0.1666666666666667684 ) ) ;
#882=DIRECTION ( 'NONE',  ( 0.000000000000000000, 0.000000000000000000, -1.000000000000000000 ) ) ;
#884=ORIENTED_EDGE ( 'NONE', *, *, #7595, .T. ) ;
#891=CARTESIAN_POINT ( 'NONE',  ( 220.0000000000000000, -56.99999999999999289, 0.000000000000000000 ) ) ;
#895=ORIENTED_EDGE ( 'NONE', *, *, #1028, .F. ) ;
#900=CARTESIAN_POINT ( 'NONE',  ( 209.9999999999999716, 3.000000000000000000, 35.00000000000000000 ) ) ;
#901=AXIS2_PLACEMENT_3D ( 'NONE', #549, #5825, #5321 ) ;
#903=CYLINDRICAL_SURFACE ( 'NONE', #5902, 8.500000000000007105 ) ;
#909=EDGE_CURVE ( 'NONE', #4559, #6005, #866, .T. ) ;
#911=EDGE_CURVE ( 'NONE', #496, #5696, #4466, .T. ) ;
#912=VECTOR ( 'NONE', #4355, 1000.000000000000000 ) ;
#915=SHAPE_REPRESENTATION ( 'base', ( #1914 ), #1662 ) ;
#922=CARTESIAN_POINT ( 'NONE',  ( 50.04196010845020481, -18.04196010845019060, 12.50000000000000533 ) ) ;
#923=ORIENTED_EDGE ( 'NONE', *, *, #603, .T. ) ;
#927=FACE_OUTER_BOUND ( 'NONE', #4248, .T. ) ;
#928=EDGE_CURVE ( 'NONE', #734, #6541, #3746, .T. ) ;
#931=ORIENTED_EDGE ( 'NONE', *, *, #6269, .T. ) ;
#933=DIRECTION ( 'NONE',  ( 0.000000000000000000, 0.9993908270190955401, -0.03489949670250403618 ) ) ;
#938=ORIENTED_EDGE ( 'NONE', *, *, #275, .F. ) ;
#939=VECTOR ( 'NONE', #6062, 1000.000000000000000 ) ;
#941=EDGE_CURVE ( 'NONE', #7205, #6206, #3855, .T. ) ;
#943=CARTESIAN_POINT ( 'NONE',  ( 186.9765770670147447, 7.979251100714891187, 15.12226171595996149 ) ) ;
#945=DIRECTION ( 'NONE',  ( -1.000000000000000000, -0.000000000000000000, -0.000000000000000000 ) ) ;
#946=CARTESIAN_POINT ( 'NONE',  ( 50.00000000000000000, -24.98477067547739239, 35.87248741756260983 ) ) ;
#950=ORIENTED_EDGE ( 'NONE', *, *, #7157, .F. ) ;
#966=ORIENTED_EDGE ( 'NONE', *, *, #4995, .F. ) ;
#969=CARTESIAN_POINT ( 'NONE',  ( 50.00000000000000000, 21.91628335801839711, 36.91742634044857141 ) ) ;
#971=EDGE_CURVE ( 'NONE', #5359, #6935, #5515, .T. ) ;
#976=CIRCLE ( 'NONE', #3193, 2.999999999999999112 ) ;
#979=CARTESIAN_POINT ( 'NONE',  ( 187.2209104841768124, -6.851359138792246561, 15.00000000000000711 ) ) ;
#982=AXIS2_PLACEMENT_3D ( 'NONE', #863, #1942, #3028 ) ;
#983=EDGE_CURVE ( 'NONE', #5743, #7468, #3337, .T. ) ;
#984=EDGE_CURVE ( 'NONE', #7571, #2976, #4548, .T. ) ;
#986=ORIENTED_EDGE ( 'NONE', *, *, #3814, .F. ) ;
#988=DIRECTION ( 'NONE',  ( 0.000000000000000000, 0.000000000000000000, 1.000000000000000000 ) ) ;
#990=DIRECTION ( 'NONE',  ( 0.000000000000000000, 0.000000000000000000, 1.000000000000000000 ) ) ;
#991=CARTESIAN_POINT ( 'NONE',  ( 217.0000000000000000, 9.000000000000001776, 18.00000000000001066 ) ) ;
#995=VECTOR ( 'NONE', #3968, 1000.000000000000000 ) ;
#996=ORIENTED_EDGE ( 'NONE', *, *, #667, .T. ) ;
#997=CARTESIAN_POINT ( 'NONE',  ( 217.0000000000000000, -18.04196010845019060, 12.50000000000000711 ) ) ;
#999=CARTESIAN_POINT ( 'NONE',  ( 49.62135916575813610, -24.29528608451959570, 12.94727185322461871 ) ) ;
#1005=ORIENTED_EDGE ( 'NONE', *, *, #6146, .T. ) ;
#1014=CARTESIAN_POINT ( 'NONE',  ( 186.9059892324150383, 5.031373033403108153, 15.00000000000000888 ) ) ;
#1015=AXIS2_PLACEMENT_3D ( 'NONE', #5249, #7129, #4136 ) ;
#1016=CARTESIAN_POINT ( 'NONE',  ( 186.1227768564662028, 7.475225542043804516, 13.64343637173987922 ) ) ;
#1018=DIRECTION ( 'NONE',  ( 1.000000000000000000, 0.000000000000000000, 0.000000000000000000 ) ) ;
#1022=VECTOR ( 'NONE', #4733, 1000.000000000000000 ) ;
#1028=EDGE_CURVE ( 'NONE', #5645, #3, #463, .T. ) ;
#1031=ORIENTED_EDGE ( 'NONE', *, *, #7385, .F. ) ;
#1035=CIRCLE ( 'NONE', #671, 8.500000000000007105 ) ;
#1036=DIRECTION ( 'NONE',  ( -0.000000000000000000, -1.000000000000000000, -0.000000000000000000 ) ) ;
#1037=EDGE_CURVE ( 'NONE', #4091, #6371, #5300, .T. ) ;
#1038=ORIENTED_EDGE ( 'NONE', *, *, #1220, .F. ) ;
#1044=ORIENTED_EDGE ( 'NONE', *, *, #682, .F. ) ;
#1046=ORIENTED_EDGE ( 'NONE', *, *, #1617, .F. ) ;
#1049=CYLINDRICAL_SURFACE ( 'NONE', #5542, 2.999999999999999112 ) ;
#1050=CARTESIAN_POINT ( 'NONE',  ( 47.00000000000000000, -25.78715168812825098, 12.89530150989249435 ) ) ;
#1054=CARTESIAN_POINT ( 'NONE',  ( 50.01335591787553625, 18.01335591787552559, 12.66922467357069770 ) ) ;
#1064=CARTESIAN_POINT ( 'NONE',  ( 3.000000000000002665, 56.99999999999999289, 3.000000000000021760 ) ) ;
#1065=CARTESIAN_POINT ( 'NONE',  ( 217.0000000000000000, -20.99999999999999645, 10.00000000000000888 ) ) ;
#1067=CARTESIAN_POINT ( 'NONE',  ( 186.9059892324150383, 6.000000000000000000, 15.00000000000000888 ) ) ;
#1073=ORIENTED_EDGE ( 'NONE', *, *, #5268, .T. ) ;
#1078=DIRECTION ( 'NONE',  ( 1.000000000000000000, 0.000000000000000000, 0.000000000000000000 ) ) ;
#1082=EDGE_CURVE ( 'NONE', #647, #1980, #1440, .T. ) ;
#1083=CARTESIAN_POINT ( 'NONE',  ( 53.00000000000547118, 24.79732742385519018, 10.00000000000000888 ) ) ;
#1084=ORIENTED_EDGE ( 'NONE', *, *, #3702, .T. ) ;
#1087=DIRECTION ( 'NONE',  ( 0.000000000000000000, 0.000000000000000000, -1.000000000000000000 ) ) ;
#1088=ORIENTED_EDGE ( 'NONE', *, *, #4315, .T. ) ;
#1090=LINE ( 'NONE', #4564, #6603 ) ;
#1091=DIRECTION ( 'NONE',  ( 1.000000000000000000, 0.000000000000000000, 0.000000000000000000 ) ) ;
#1101=DIRECTION ( 'NONE',  ( 1.000000000000000000, -0.000000000000000000, -0.000000000000000000 ) ) ;
#1103=ADVANCED_FACE ( 'NONE', ( #6393 ), #126, .F. ) ;
#1109=ORIENTED_EDGE ( 'NONE', *, *, #7198, .T. ) ;
#1112=ADVANCED_FACE ( 'NONE', ( #1812, #1338 ), #5392, .T. ) ;
#1113=DIRECTION ( 'NONE',  ( 0.000000000000000000, 0.000000000000000000, -1.000000000000000000 ) ) ;
#1115=CARTESIAN_POINT ( 'NONE',  ( 49.99999999999999289, -22.78166690339261535, 10.00000000000000888 ) ) ;
#1117=AXIS2_PLACEMENT_3D ( 'NONE', #3313, #1426, #845 ) ;
#1125=DIRECTION ( 'NONE',  ( 1.000000000000000000, 0.000000000000000000, 0.000000000000000000 ) ) ;
#1137=DIRECTION ( 'NONE',  ( 1.000000000000000000, 0.000000000000000000, 0.000000000000000000 ) ) ;
#1138=DIRECTION ( 'NONE',  ( 0.000000000000000000, 0.000000000000000000, -1.000000000000000000 ) ) ;
#1140=VERTEX_POINT ( 'NONE', #1307 ) ;
#1144=DIRECTION ( 'NONE',  ( 1.000000000000000000, 0.000000000000000000, 0.000000000000000000 ) ) ;
#1147=CIRCLE ( 'NONE', #6443, 8.500000000000007105 ) ;
#1148=ORIENTED_EDGE ( 'NONE', *, *, #841, .T. ) ;
#1155=ORIENTED_EDGE ( 'NONE', *, *, #7521, .T. ) ;
#1161=CARTESIAN_POINT ( 'NONE',  ( 217.0000000000000000, 6.000000000000000000, 18.00000000000001066 ) ) ;
#1162=VECTOR ( 'NONE', #3026, 1000.000000000000000 ) ;
#1179=CARTESIAN_POINT ( 'NONE',  ( 193.5000000000000000, -39.99999999999999289, 0.000000000000000000 ) ) ;
#1183=EDGE_LOOP ( 'NONE', ( #3146, #1369, #7460, #5155 ) ) ;
#1184=ORIENTED_EDGE ( 'NONE', *, *, #5395, .T. ) ;
#1190=CARTESIAN_POINT ( 'NONE',  ( 46.99999999999999289, -28.78532416918554304, 10.00000000000000533 ) ) ;
#1199=DIRECTION ( 'NONE',  ( 1.000000000000000000, 0.000000000000000000, 0.000000000000000000 ) ) ;
#1207=CARTESIAN_POINT ( 'NONE',  ( 53.00000000000000711, 24.00878702352406435, 10.00000000000001066 ) ) ;
#1208=ADVANCED_FACE ( 'NONE', ( #5540 ), #5888, .T. ) ;
#1214=LINE ( 'NONE', #5910, #5739 ) ;
#1216=CARTESIAN_POINT ( 'NONE',  ( 220.0000000000000000, -18.00000000000000000, 10.00000000000000888 ) ) ;
#1217=DIRECTION ( 'NONE',  ( 0.000000000000000000, -0.000000000000000000, -1.000000000000000000 ) ) ;
#1218=CARTESIAN_POINT ( 'NONE',  ( 0.000000000000000000, 30.03170604878415162, 13.00000000000001066 ) ) ;
#1220=EDGE_CURVE ( 'NONE', #2238, #5445, #803, .T. ) ;
#1221=EDGE_LOOP ( 'NONE', ( #3013, #2785, #6919, #6312, #4124 ) ) ;
#1222=ORIENTED_EDGE ( 'NONE', *, *, #2363, .F. ) ;
#1223=CARTESIAN_POINT ( 'NONE',  ( 188.6380400399839061, -9.000000000000001776, 15.00000000000000888 ) ) ;
#1225=AXIS2_PLACEMENT_3D ( 'NONE', #2444, #174, #7102 ) ;
#1230=CARTESIAN_POINT ( 'NONE',  ( 3.000000000000002665, -56.99999999999999289, 10.00000000000000000 ) ) ;
#1231=VERTEX_POINT ( 'NONE', #267 ) ;
#1232=AXIS2_PLACEMENT_3D ( 'NONE', #447, #6214, #3375 ) ;
#1234=CARTESIAN_POINT ( 'NONE',  ( 0.000000000000000000, -56.99999999999999289, 7.000000000000000888 ) ) ;
#1238=AXIS2_PLACEMENT_3D ( 'NONE', #4836, #4909, #1903 ) ;
#1243=CIRCLE ( 'NONE', #5547, 2.999999999999999112 ) ;
#1249=CARTESIAN_POINT ( 'NONE',  ( 217.0000000000000000, 60.00000000000000000, 10.00000000000002309 ) ) ;
#1255=FACE_OUTER_BOUND ( 'NONE', #4425, .T. ) ;
#1260=ORIENTED_EDGE ( 'NONE', *, *, #3630, .F. ) ;
#1261=ADVANCED_FACE ( 'NONE', ( #7108 ), #6604, .T. ) ;
#1275=EDGE_CURVE ( 'NONE', #3543, #5645, #714, .T. ) ;
#1276=CARTESIAN_POINT ( 'NONE',  ( 220.0000000000000000, 18.04196010845019060, 12.50000000000000711 ) ) ;
#1277=FACE_OUTER_BOUND ( 'NONE', #2513, .T. ) ;
#1278=AXIS2_PLACEMENT_3D ( 'NONE', #3049, #5641, #764 ) ;
#1280=ORIENTED_EDGE ( 'NONE', *, *, #5374, .F. ) ;
#1285=AXIS2_PLACEMENT_3D ( 'NONE', #3678, #6666, #6094 ) ;
#1288=CARTESIAN_POINT ( 'NONE',  ( 176.5000000000000000, 39.99999999999999289, 10.00000000000000355 ) ) ;
#1289=CARTESIAN_POINT ( 'NONE',  ( 51.46767767233085067, 19.46767767233084712, 10.00000000000001066 ) ) ;
#1290=AXIS2_PLACEMENT_3D ( 'NONE', #5768, #2837, #6960 ) ;
#1291=AXIS2_PLACEMENT_3D ( 'NONE', #2963, #2849, #4049 ) ;
#1294=FACE_OUTER_BOUND ( 'NONE', #3045, .T. ) ;
#1298=CARTESIAN_POINT ( 'NONE',  ( 188.5973441732890308, -3.156163941073441226, 17.92951269122647062 ) ) ;
#1307=CARTESIAN_POINT ( 'NONE',  ( 3.000000000000002665, 56.99999999999999289, 2.149255132503604690E-14 ) ) ;
#1309=ORIENTED_EDGE ( 'NONE', *, *, #1788, .F. ) ;
#1310=VERTEX_POINT ( 'NONE', #788 ) ;
#1311=VECTOR ( 'NONE', #6828, 1000.000000000000000 ) ;
#1312=DIRECTION ( 'NONE',  ( 0.000000000000000000, -1.000000000000000000, -0.000000000000000000 ) ) ;
#1317=EDGE_CURVE ( 'NONE', #1140, #496, #5984, .T. ) ;
#1318=ADVANCED_FACE ( 'NONE', ( #1294 ), #4222, .T. ) ;
#1319=ORIENTED_EDGE ( 'NONE', *, *, #5713, .T. ) ;
#1328=DIRECTION ( 'NONE',  ( 1.000000000000000000, 0.000000000000000000, 0.000000000000000000 ) ) ;
#1336=DIRECTION ( 'NONE',  ( 0.000000000000000000, -0.9961946980917452121, -0.08715574274766277330 ) ) ;
#1338=FACE_BOUND ( 'NONE', #2294, .T. ) ;
#1341=EDGE_LOOP ( 'NONE', ( #3669, #5770, #2012, #1859 ) ) ;
#1343=LINE ( 'NONE', #2391, #7296 ) ;
#1345=VERTEX_POINT ( 'NONE', #5990 ) ;
#1346=FACE_OUTER_BOUND ( 'NONE', #6166, .T. ) ;
#1348=AXIS2_PLACEMENT_3D ( 'NONE', #2791, #2179, #7293 ) ;
#1349=ORIENTED_EDGE ( 'NONE', *, *, #2802, .T. ) ;
#1350=CARTESIAN_POINT ( 'NONE',  ( 189.5040654437683258, 3.000000000000000000, 19.50000000000000711 ) ) ;
#1353=CARTESIAN_POINT ( 'NONE',  ( 3.000000000000002665, 0.000000000000000000, 60.00000000000000711 ) ) ;
#1354=ORIENTED_EDGE ( 'NONE', *, *, #7198, .F. ) ;
#1356=DIRECTION ( 'NONE',  ( 0.000000000000000000, 0.08715574274766212104, -0.9961946980917452121 ) ) ;
#1360=EDGE_CURVE ( 'NONE', #4415, #6542, #7573, .T. ) ;
#1363=DIRECTION ( 'NONE',  ( 0.000000000000000000, 0.000000000000000000, -1.000000000000000000 ) ) ;
#1366=CARTESIAN_POINT ( 'NONE',  ( 186.9059892324150383, -5.031373033403107264, 15.00000000000000888 ) ) ;
#1367=CIRCLE ( 'NONE', #4942, 3.000000000000000000 ) ;
#1368=ORIENTED_EDGE ( 'NONE', *, *, #1275, .T. ) ;
#1369=ORIENTED_EDGE ( 'NONE', *, *, #7147, .F. ) ;
#1372=CARTESIAN_POINT ( 'NONE',  ( 217.0000000000000000, 20.99999999999999645, 13.00000000000000888 ) ) ;
#1373=CARTESIAN_POINT ( 'NONE',  ( 216.9999999999999716, -6.000000000000000000, 35.00000000000000000 ) ) ;
#1376=EDGE_CURVE ( 'NONE', #5743, #6273, #1214, .T. ) ;
#1382=CARTESIAN_POINT ( 'NONE',  ( 49.99999999999998579, -20.99999999999999645, 10.00000000000000888 ) ) ;
#1385=AXIS2_PLACEMENT_3D ( 'NONE', #2667, #5669, #471 ) ;
#1386=CARTESIAN_POINT ( 'NONE',  ( 50.00000000000000000, 1.714505518806293455E-15, 21.00000000000001066 ) ) ;
#1387=CARTESIAN_POINT ( 'NONE',  ( 48.75735931288071612, 27.04312195450891565, 12.73853277175702381 ) ) ;
#1391=CYLINDRICAL_SURFACE ( 'NONE', #2109, 3.000000000000000000 ) ;
#1398=VECTOR ( 'NONE', #6177, 1000.000000000000000 ) ;
#1400=DIRECTION ( 'NONE',  ( -0.000000000000000000, 0.03489949670250429292, 0.9993908270190956511 ) ) ;
#1405=EDGE_LOOP ( 'NONE', ( #7002, #847, #4554, #7311 ) ) ;
#1407=AXIS2_PLACEMENT_3D ( 'NONE', #3227, #3808, #1336 ) ;
#1421=VERTEX_POINT ( 'NONE', #5059 ) ;
#1422=VECTOR ( 'NONE', #1101, 1000.000000000000000 ) ;
#1426=DIRECTION ( 'NONE',  ( -0.000000000000000000, 1.000000000000000000, 0.000000000000000000 ) ) ;
#1427=EDGE_LOOP ( 'NONE', ( #2871, #966 ) ) ;
#1428=AXIS2_PLACEMENT_3D ( 'NONE', #5378, #2449, #3651 ) ;
#1432=CARTESIAN_POINT ( 'NONE',  ( 35.00000000000000000, 39.99999999999999289, 0.000000000000000000 ) ) ;
#1435=CARTESIAN_POINT ( 'NONE',  ( 50.00000000000000000, 0.000000000000000000, 35.00000000000000000 ) ) ;
#1437=CARTESIAN_POINT ( 'NONE',  ( 220.0000000000000000, 3.000000000000000000, 18.00000000000001066 ) ) ;
#1440=( BOUNDED_CURVE ( )  B_SPLINE_CURVE ( 3, ( #1653, #576, #4011, #3356 ),
 .UNSPECIFIED., .F., .T. ) 
 B_SPLINE_CURVE_WITH_KNOTS ( ( 4, 4 ),
 ( 4.712388980384689674, 6.283185307179586232 ),
 .UNSPECIFIED. ) 
 CURVE ( )  GEOMETRIC_REPRESENTATION_ITEM ( )  RATIONAL_B_SPLINE_CURVE ( ( 1.000000000000000000, 0.8047378541243649375, 0.8047378541243649375, 1.000000000000000000 ) ) 
 REPRESENTATION_ITEM ( '' )  );
#1443=DIRECTION ( 'NONE',  ( 0.000000000000000000, 0.000000000000000000, -1.000000000000000000 ) ) ;
#1444=DIRECTION ( 'NONE',  ( -0.8660254037844410391, 0.000000000000000000, 0.4999999999999959477 ) ) ;
#1446=CARTESIAN_POINT ( 'NONE',  ( 187.1032291023277025, -6.494931230503832253, 15.00000000000001066 ) ) ;
#1451=CARTESIAN_POINT ( 'NONE',  ( 220.0000000000000000, -56.99999999999999289, 3.000000000000000000 ) ) ;
#1452=EDGE_CURVE ( 'NONE', #5563, #529, #7331, .T. ) ;
#1455=ORIENTED_EDGE ( 'NONE', *, *, #1775, .T. ) ;
#1456=CARTESIAN_POINT ( 'NONE',  ( 50.00000000000000000, 0.000000000000000000, 35.00000000000000000 ) ) ;
#1457=EDGE_CURVE ( 'NONE', #5033, #1231, #2417, .T. ) ;
#1458=ORIENTED_EDGE ( 'NONE', *, *, #4075, .F. ) ;
#1459=DIRECTION ( 'NONE',  ( -1.000000000000000000, -0.000000000000000000, -0.000000000000000000 ) ) ;
#1460=DIRECTION ( 'NONE',  ( 0.000000000000000000, 0.000000000000000000, -1.000000000000000000 ) ) ;
#1463=CARTESIAN_POINT ( 'NONE',  ( 47.39276988301191551, 27.04312195450870249, 12.73853277175948939 ) ) ;
#1465=VERTEX_POINT ( 'NONE', #1549 ) ;
#1469=AXIS2_PLACEMENT_3D ( 'NONE', #676, #4800, #5944 ) ;
#1471=EDGE_CURVE ( 'NONE', #6371, #510, #3158, .T. ) ;
#1472=AXIS2_PLACEMENT_3D ( 'NONE', #2291, #4057, #4557 ) ;
#1474=DIRECTION ( 'NONE',  ( 0.000000000000000000, 0.000000000000000000, 1.000000000000000000 ) ) ;
#1475=DIRECTION ( 'NONE',  ( -1.000000000000000000, -0.000000000000000000, -0.000000000000000000 ) ) ;
#1477=CARTESIAN_POINT ( 'NONE',  ( 186.9059892324150098, -5.404540004443668444, 15.00000000000001066 ) ) ;
#1485=DIRECTION ( 'NONE',  ( 1.000000000000000000, 0.000000000000000000, 0.000000000000000000 ) ) ;
#1486=ORIENTED_EDGE ( 'NONE', *, *, #4286, .F. ) ;
#1487=EDGE_CURVE ( 'NONE', #1645, #7378, #6246, .T. ) ;
#1489=CIRCLE ( 'NONE', #2723, 6.000000000000019540 ) ;
#1490=DIRECTION ( 'NONE',  ( 0.000000000000000000, 0.000000000000000000, 1.000000000000000000 ) ) ;
#1491=EDGE_LOOP ( 'NONE', ( #530, #5499, #1046, #2119, #1309 ) ) ;
#1497=CARTESIAN_POINT ( 'NONE',  ( 48.61993474911651703, 26.84407407967428938, 10.00000000000000888 ) ) ;
#1499=ORIENTED_EDGE ( 'NONE', *, *, #3942, .T. ) ;
#1500=DIRECTION ( 'NONE',  ( -0.000000000000000000, 0.03489949670250429292, 0.9993908270190955401 ) ) ;
#1506=ORIENTED_EDGE ( 'NONE', *, *, #4001, .T. ) ;
#1507=CARTESIAN_POINT ( 'NONE',  ( 47.00000000000000000, -21.98659819442010743, 35.76778892745510063 ) ) ;
#1511=CARTESIAN_POINT ( 'NONE',  ( 186.0401176793982074, 9.056547830598860926, 13.50026647734630281 ) ) ;
#1514=FACE_OUTER_BOUND ( 'NONE', #202, .T. ) ;
#1516=EDGE_LOOP ( 'NONE', ( #451, #6770, #5098, #2128 ) ) ;
#1521=EDGE_CURVE ( 'NONE', #3769, #2238, #3780, .T. ) ;
#1524=AXIS2_PLACEMENT_3D ( 'NONE', #7321, #1614, #6276 ) ;
#1527=AXIS2_PLACEMENT_3D ( 'NONE', #1230, #3589, #653 ) ;
#1537=CARTESIAN_POINT ( 'NONE',  ( 47.84883112649161774, 27.19103684831782530, 10.00000000000000711 ) ) ;
#1544=ADVANCED_FACE ( 'NONE', ( #3294 ), #4446, .T. ) ;
#1545=FACE_OUTER_BOUND ( 'NONE', #4931, .T. ) ;
#1546=AXIS2_PLACEMENT_3D ( 'NONE', #2070, #7374, #4419 ) ;
#1547=EDGE_LOOP ( 'NONE', ( #4430, #3821, #617, #1874, #2822, #3351, #5883, #4240, #544, #1084 ) ) ;
#1549=CARTESIAN_POINT ( 'NONE',  ( 50.00000000000000000, 1.714505518806293455E-15, 21.00000000000001066 ) ) ;
#1554=LINE ( 'NONE', #5639, #6755 ) ;
#1557=CIRCLE ( 'NONE', #99, 3.000000000000004885 ) ;
#1562=CARTESIAN_POINT ( 'NONE',  ( 3.000000000000002665, -56.99999999999999289, 7.000000000000000888 ) ) ;
#1563=FACE_OUTER_BOUND ( 'NONE', #3181, .T. ) ;
#1566=EDGE_CURVE ( 'NONE', #734, #7349, #5867, .T. ) ;
#1574=CARTESIAN_POINT ( 'NONE',  ( 49.99999999999999289, 24.40605214882040741, 12.96576784911518487 ) ) ;
#1575=FACE_OUTER_BOUND ( 'NONE', #2891, .T. ) ;
#1576=EDGE_LOOP ( 'NONE', ( #7215, #2234, #6124, #117 ) ) ;
#1581=EDGE_LOOP ( 'NONE', ( #4770, #7299, #6612, #7498 ) ) ;
#1583=EDGE_CURVE ( 'NONE', #4590, #5645, #3785, .T. ) ;
#1587=CARTESIAN_POINT ( 'NONE',  ( 187.4728481691300885, 6.631203003894613701, 15.98182847912006643 ) ) ;
#1590=CARTESIAN_POINT ( 'NONE',  ( 203.9378221735088914, -3.000000000000000888, 38.49999999999998579 ) ) ;
#1593=ORIENTED_EDGE ( 'NONE', *, *, #7417, .T. ) ;
#1596=LINE ( 'NONE', #1635, #2511 ) ;
#1602=CIRCLE ( 'NONE', #5907, 25.00000000000000000 ) ;
#1603=DIRECTION ( 'NONE',  ( 0.000000000000000000, -1.000000000000000000, -2.065146995210484941E-16 ) ) ;
#1604=VERTEX_POINT ( 'NONE', #2861 ) ;
#1614=DIRECTION ( 'NONE',  ( 0.000000000000000000, 3.304235192336776498E-16, -1.000000000000000000 ) ) ;
#1617=EDGE_CURVE ( 'NONE', #4614, #5055, #5431, .T. ) ;
#1619=FACE_OUTER_BOUND ( 'NONE', #6981, .T. ) ;
#1622=ORIENTED_EDGE ( 'NONE', *, *, #3151, .F. ) ;
#1625=EDGE_CURVE ( 'NONE', #4590, #6224, #1090, .T. ) ;
#1629=ADVANCED_FACE ( 'NONE', ( #5792 ), #5139, .F. ) ;
#1632=CIRCLE ( 'NONE', #7532, 2.999999999999999556 ) ;
#1634=VERTEX_POINT ( 'NONE', #3983 ) ;
#1635=CARTESIAN_POINT ( 'NONE',  ( 220.0000000000000000, 60.00000000000000000, 7.000000000000022204 ) ) ;
#1636=PLANE ( 'NONE',  #1865 ) ;
#1638=LINE ( 'NONE', #1067, #5349 ) ;
#1641=CIRCLE ( 'NONE', #7176, 3.000000000000000000 ) ;
#1642=EDGE_CURVE ( 'NONE', #6541, #5934, #3416, .T. ) ;
#1644=PRODUCT_DEFINITION ( 'UNKNOWN', '', #7435, #5946 ) ;
#1645=VERTEX_POINT ( 'NONE', #476 ) ;
#1649=AXIS2_PLACEMENT_3D ( 'NONE', #6016, #742, #817 ) ;
#1650=DIRECTION ( 'NONE',  ( 0.000000000000000000, 0.000000000000000000, 1.000000000000000000 ) ) ;
#1651=CARTESIAN_POINT ( 'NONE',  ( 217.0000000000000000, 20.99999999999999645, 10.00000000000001066 ) ) ;
#1652=VERTEX_POINT ( 'NONE', #7443 ) ;
#1653=CARTESIAN_POINT ( 'NONE',  ( 192.1021416551216419, -6.000000000000000000, 18.00000000000001066 ) ) ;
#1654=DIRECTION ( 'NONE',  ( 0.000000000000000000, 0.000000000000000000, -1.000000000000000000 ) ) ;
#1655=AXIS2_PLACEMENT_3D ( 'NONE', #2229, #3923, #3999 ) ;
#1657=VECTOR ( 'NONE', #1475, 1000.000000000000000 ) ;
#1658=( BOUNDED_CURVE ( )  B_SPLINE_CURVE ( 3, ( #7109, #3535, #7562, #2303 ),
 .UNSPECIFIED., .F., .T. ) 
 B_SPLINE_CURVE_WITH_KNOTS ( ( 4, 4 ),
 ( 0.7227342478134169967, 1.570796326794897002 ),
 .UNSPECIFIED. ) 
 CURVE ( )  GEOMETRIC_REPRESENTATION_ITEM ( )  RATIONAL_B_SPLINE_CURVE ( ( 1.000000000000000000, 0.9409585518440986007, 0.9409585518440986007, 1.000000000000000000 ) ) 
 REPRESENTATION_ITEM ( '' )  );
#1660=CARTESIAN_POINT ( 'NONE',  ( 50.03402421525600374, 24.40363903897386422, 9.999999999997291056 ) ) ;
#1662=( GEOMETRIC_REPRESENTATION_CONTEXT ( 3 ) GLOBAL_UNCERTAINTY_ASSIGNED_CONTEXT ( ( #3425 ) ) GLOBAL_UNIT_ASSIGNED_CONTEXT ( ( #632, #3486, #5941 ) ) REPRESENTATION_CONTEXT ( 'NONE', 'WORKASPACE' ) );
#1673=CARTESIAN_POINT ( 'NONE',  ( 217.0000000000000000, 60.00000000000000000, 7.000000000000022204 ) ) ;
#1678=ORIENTED_EDGE ( 'NONE', *, *, #5058, .F. ) ;
#1679=VECTOR ( 'NONE', #3775, 1000.000000000000000 ) ;
#1684=LINE ( 'NONE', #6959, #4114 ) ;
#1685=CARTESIAN_POINT ( 'NONE',  ( 220.0000000000000000, 56.99999999999999289, 7.000000000000022204 ) ) ;
#1686=CARTESIAN_POINT ( 'NONE',  ( 188.7282013335461670, -8.214756345321047704, 15.07808197065826405 ) ) ;
#1687=AXIS2_PLACEMENT_3D ( 'NONE', #2806, #3753, #243 ) ;
#1688=ORIENTED_EDGE ( 'NONE', *, *, #219, .T. ) ;
#1689=ORIENTED_EDGE ( 'NONE', *, *, #3447, .T. ) ;
#1692=CARTESIAN_POINT ( 'NONE',  ( 220.0000000000000000, -9.000000000000001776, 18.00000000000001066 ) ) ;
#1693=ORIENTED_EDGE ( 'NONE', *, *, #2515, .F. ) ;
#1698=ADVANCED_FACE ( 'NONE', ( #3482 ), #399, .F. ) ;
#1700=DIRECTION ( 'NONE',  ( -0.000000000000000000, 0.000000000000000000, 1.000000000000000000 ) ) ;
#1701=EDGE_LOOP ( 'NONE', ( #4907, #4460, #2033, #5024 ) ) ;
#1710=CARTESIAN_POINT ( 'NONE',  ( 3.000000000000002665, -60.00000000000000000, 10.00000000000000000 ) ) ;
#1711=LINE ( 'NONE', #7063, #4189 ) ;
#1715=LINE ( 'NONE', #6676, #5465 ) ;
#1716=DIRECTION ( 'NONE',  ( 0.000000000000000000, 1.836970198721029934E-16, -1.000000000000000000 ) ) ;
#1721=AXIS2_PLACEMENT_3D ( 'NONE', #6754, #295, #6066 ) ;
#1731=VECTOR ( 'NONE', #6187, 1000.000000000000000 ) ;
#1739=DIRECTION ( 'NONE',  ( 0.4999999999999976130, 0.000000000000000000, 0.8660254037844399289 ) ) ;
#1740=CARTESIAN_POINT ( 'NONE',  ( 217.0000000000000000, 56.99999999999999289, 7.000000000000022204 ) ) ;
#1741=EDGE_CURVE ( 'NONE', #3993, #4453, #2309, .T. ) ;
#1747=DIRECTION ( 'NONE',  ( -0.000000000000000000, 0.000000000000000000, 1.000000000000000000 ) ) ;
#1749=CARTESIAN_POINT ( 'NONE',  ( 0.000000000000000000, 0.000000000000000000, 0.000000000000000000 ) ) ;
#1752=CARTESIAN_POINT ( 'NONE',  ( 192.1021416551216419, 6.000000000000000000, 18.00000000000001066 ) ) ;
#1765=CYLINDRICAL_SURFACE ( 'NONE', #1772, 2.999999999999999112 ) ;
#1770=CYLINDRICAL_SURFACE ( 'NONE', #1291, 2.999999999999999112 ) ;
#1772=AXIS2_PLACEMENT_3D ( 'NONE', #4123, #6505, #6467 ) ;
#1773=AXIS2_PLACEMENT_3D ( 'NONE', #5983, #6629, #3169 ) ;
#1774=ORIENTED_EDGE ( 'NONE', *, *, #5786, .F. ) ;
#1775=EDGE_CURVE ( 'NONE', #429, #233, #2403, .T. ) ;
#1777=CARTESIAN_POINT ( 'NONE',  ( 217.0000000000000000, -56.99999999999999289, 10.00000000000000000 ) ) ;
#1783=DIRECTION ( 'NONE',  ( -0.000000000000000000, 0.000000000000000000, 1.000000000000000000 ) ) ;
#1788=EDGE_CURVE ( 'NONE', #722, #2384, #3677, .T. ) ;
#1797=DIRECTION ( 'NONE',  ( 1.000000000000000000, 0.000000000000000000, 0.000000000000000000 ) ) ;
#1800=FACE_BOUND ( 'NONE', #225, .T. ) ;
#1801=DIRECTION ( 'NONE',  ( -0.4999999999999976130, -0.000000000000000000, -0.8660254037844399289 ) ) ;
#1805=ORIENTED_EDGE ( 'NONE', *, *, #941, .F. ) ;
#1812=FACE_OUTER_BOUND ( 'NONE', #407, .T. ) ;
#1813=CARTESIAN_POINT ( 'NONE',  ( 50.00000000000000000, 0.000000000000000000, 35.00000000000000000 ) ) ;
#1814=EDGE_CURVE ( 'NONE', #2614, #2574, #7462, .T. ) ;
#1819=CARTESIAN_POINT ( 'NONE',  ( 3.000000000000000000, -56.99999999999999289, 7.000000000000000888 ) ) ;
#1820=ORIENTED_EDGE ( 'NONE', *, *, #80, .F. ) ;
#1821=CARTESIAN_POINT ( 'NONE',  ( 217.0000000000000000, -9.000000000000001776, 15.00000000000000888 ) ) ;
#1822=FACE_OUTER_BOUND ( 'NONE', #2715, .T. ) ;
#1823=EDGE_LOOP ( 'NONE', ( #1349, #2669, #262, #1678 ) ) ;
#1828=CARTESIAN_POINT ( 'NONE',  ( 3.000000000000002665, 60.00000000000000000, 7.000000000000023093 ) ) ;
#1829=ADVANCED_FACE ( 'NONE', ( #4217, #170 ), #5405, .F. ) ;
#1830=B_SPLINE_CURVE_WITH_KNOTS ( 'NONE', 3,
 ( #922, #2078, #5620, #343 ),
 .UNSPECIFIED., .F., .F.,
 ( 4, 4 ),
 ( 1.734723475976807094E-18, 0.0005182278649586899693 ),
 .UNSPECIFIED. ) ;
#1832=CARTESIAN_POINT ( 'NONE',  ( 220.0000000000000000, 20.99999999999999645, 7.000000000000009770 ) ) ;
#1834=CARTESIAN_POINT ( 'NONE',  ( 186.9059892324150951, 5.404544942268280749, 15.00000000000001421 ) ) ;
#1837=ORIENTED_EDGE ( 'NONE', *, *, #2696, .T. ) ;
#1838=EDGE_LOOP ( 'NONE', ( #7165, #4210, #1368, #153 ) ) ;
#1839=EDGE_CURVE ( 'NONE', #647, #1652, #1557, .T. ) ;
#1854=ORIENTED_EDGE ( 'NONE', *, *, #4508, .T. ) ;
#1859=ORIENTED_EDGE ( 'NONE', *, *, #124, .F. ) ;
#1862=ADVANCED_FACE ( 'NONE', ( #927, #3283, #6092, #5738, #460 ), #816, .F. ) ;
#1864=DIRECTION ( 'NONE',  ( 1.000000000000000000, 0.000000000000000000, 0.000000000000000000 ) ) ;
#1865=AXIS2_PLACEMENT_3D ( 'NONE', #1216, #3996, #3572 ) ;
#1872=CYLINDRICAL_SURFACE ( 'NONE', #2361, 3.000000000000001332 ) ;
#1873=CARTESIAN_POINT ( 'NONE',  ( 188.3801170496620045, 8.732029405377334186, 15.00000000000001066 ) ) ;
#1874=ORIENTED_EDGE ( 'NONE', *, *, #3382, .T. ) ;
#1878=EDGE_CURVE ( 'NONE', #1465, #3492, #4435, .T. ) ;
#1881=AXIS2_PLACEMENT_3D ( 'NONE', #98, #2360, #3522 ) ;
#1883=DIRECTION ( 'NONE',  ( 1.000000000000000000, 0.000000000000000000, 0.000000000000000000 ) ) ;
#1885=ORIENTED_EDGE ( 'NONE', *, *, #2468, .T. ) ;
#1887=DIRECTION ( 'NONE',  ( 1.000000000000000000, 0.000000000000000000, 0.000000000000000000 ) ) ;
#1890=ORIENTED_EDGE ( 'NONE', *, *, #6093, .T. ) ;
#1891=CARTESIAN_POINT ( 'NONE',  ( 217.0000000000000000, -9.000000000000001776, 12.00000000000000711 ) ) ;
#1892=CARTESIAN_POINT ( 'NONE',  ( 220.0000000000000000, 0.000000000000000000, 0.000000000000000000 ) ) ;
#1894=TOROIDAL_SURFACE ( 'NONE', #2878, 6.000000000000000000, 3.000000000000000000 ) ;
#1895=VERTEX_POINT ( 'NONE', #6777 ) ;
#1903=DIRECTION ( 'NONE',  ( 1.000000000000000000, 0.000000000000000000, 0.000000000000000000 ) ) ;
#1906=AXIS2_PLACEMENT_3D ( 'NONE', #3315, #6152, #882 ) ;
#1907=AXIS2_PLACEMENT_3D ( 'NONE', #900, #3763, #3143 ) ;
#1908=EDGE_CURVE ( 'NONE', #5322, #5661, #4366, .T. ) ;
#1909=ORIENTED_EDGE ( 'NONE', *, *, #5767, .F. ) ;
#1914=AXIS2_PLACEMENT_3D ( 'NONE', #1749, #62, #1864 ) ;
#1915=CARTESIAN_POINT ( 'NONE',  ( 187.9926472795798702, -6.022797726957934472, 16.88214694814191219 ) ) ;
#1920=FACE_OUTER_BOUND ( 'NONE', #415, .T. ) ;
#1932=VERTEX_POINT ( 'NONE', #1350 ) ;
#1933=DIRECTION ( 'NONE',  ( 0.000000000000000000, 0.000000000000000000, -1.000000000000000000 ) ) ;
#1942=DIRECTION ( 'NONE',  ( -1.000000000000000000, 0.000000000000000000, 0.000000000000000000 ) ) ;
#1945=( NAMED_UNIT ( * ) PLANE_ANGLE_UNIT ( ) SI_UNIT ( $, .RADIAN. ) );
#1952=ORIENTED_EDGE ( 'NONE', *, *, #1220, .T. ) ;
#1953=DIRECTION ( 'NONE',  ( 0.000000000000000000, 0.000000000000000000, 1.000000000000000000 ) ) ;
#1955=DIRECTION ( 'NONE',  ( 1.000000000000000000, 0.000000000000000000, 0.000000000000000000 ) ) ;
#1957=CARTESIAN_POINT ( 'NONE',  ( 50.00000000000000000, 17.91234734164656928, 13.00000000000000711 ) ) ;
#1959=ORIENTED_EDGE ( 'NONE', *, *, #5899, .F. ) ;
#1966=DIRECTION ( 'NONE',  ( 0.000000000000000000, 1.156482317317871133E-15, -1.000000000000000000 ) ) ;
#1967=CYLINDRICAL_SURFACE ( 'NONE', #431, 3.000000000000002665 ) ;
#1968=CLOSED_SHELL ( 'NONE', ( #55, #710, #7037, #5662, #747, #795, #5068, #2514, #6814, #1629, #2500, #3511, #1862, #7189, #4176, #770, #5651, #2668, #3020, #111, #1829, #1112, #1698, #5341, #4216, #6767, #398, #5, #256, #3282, #5377, #4521, #2185, #2591, #6007, #6918, #4078, #4502, #840, #4801, #4698, #2719, #2419, #2352, #6343, #568, #6673, #537, #4376, #2565, #317, #729, #4203, #1103, #367, #2066, #2498, #1544, #5573, #3584, #610, #5510, #264, #4009, #2763, #5483, #4573, #4718, #4138, #234, #3730, #1208, #1261, #2397, #6776, #3607, #4904, #3474, #3175, #550, #5699, #1318, #5695, #4604, #3615, #3887, #7473 ) ) ;
#1969=CIRCLE ( 'NONE', #3697, 8.500000000000007105 ) ;
#1980=VERTEX_POINT ( 'NONE', #1223 ) ;
#1983=LINE ( 'NONE', #5027, #1657 ) ;
#1985=ORIENTED_EDGE ( 'NONE', *, *, #327, .F. ) ;
#1987=CIRCLE ( 'NONE', #5552, 8.500000000000007105 ) ;
#1988=ORIENTED_EDGE ( 'NONE', *, *, #1583, .T. ) ;
#1992=FACE_OUTER_BOUND ( 'NONE', #2379, .T. ) ;
#1993=( BOUNDED_CURVE ( )  B_SPLINE_CURVE ( 3, ( #5906, #4768, #109, #1752 ),
 .UNSPECIFIED., .F., .T. ) 
 B_SPLINE_CURVE_WITH_KNOTS ( ( 4, 4 ),
 ( 3.141592653589793116, 4.712388980384689674 ),
 .UNSPECIFIED. ) 
 CURVE ( )  GEOMETRIC_REPRESENTATION_ITEM ( )  RATIONAL_B_SPLINE_CURVE ( ( 1.000000000000000000, 0.8047378541243649375, 0.8047378541243649375, 1.000000000000000000 ) ) 
 REPRESENTATION_ITEM ( '' )  );
#1997=VERTEX_POINT ( 'NONE', #3582 ) ;
#2010=CARTESIAN_POINT ( 'NONE',  ( 52.24271833150618960, 27.04204335853172836, 10.00000000000000888 ) ) ;
#2011=LINE ( 'NONE', #4945, #6075 ) ;
#2012=ORIENTED_EDGE ( 'NONE', *, *, #40, .F. ) ;
#2013=CARTESIAN_POINT ( 'NONE',  ( 53.00000000000000711, 24.00878702352406435, 10.00000000000001066 ) ) ;
#2015=FACE_OUTER_BOUND ( 'NONE', #1221, .T. ) ;
#2018=VECTOR ( 'NONE', #2237, 1000.000000000000000 ) ;
#2021=CIRCLE ( 'NONE', #6940, 3.000000000000000444 ) ;
#2022=DIRECTION ( 'NONE',  ( 1.000000000000000000, 0.000000000000000000, 0.000000000000000000 ) ) ;
#2023=( NAMED_UNIT ( * ) SI_UNIT ( $, .STERADIAN. ) SOLID_ANGLE_UNIT ( ) );
#2027=CARTESIAN_POINT ( 'NONE',  ( 220.0000000000000000, 20.99999999999999645, 10.00000000000001066 ) ) ;
#2031=ORIENTED_EDGE ( 'NONE', *, *, #2807, .T. ) ;
#2032=EDGE_CURVE ( 'NONE', #5020, #5755, #3662, .T. ) ;
#2033=ORIENTED_EDGE ( 'NONE', *, *, #3720, .T. ) ;
#2044=PLANE ( 'NONE',  #7188 ) ;
#2045=ORIENTED_EDGE ( 'NONE', *, *, #1360, .T. ) ;
#2050=ORIENTED_EDGE ( 'NONE', *, *, #4653, .F. ) ;
#2053=CARTESIAN_POINT ( 'NONE',  ( 185.0000000000000000, 39.99999999999999289, 0.000000000000000000 ) ) ;
#2062=CARTESIAN_POINT ( 'NONE',  ( 50.00000000000001421, 15.08392021690038121, 12.00000000000000711 ) ) ;
#2065=CARTESIAN_POINT ( 'NONE',  ( 50.00000000000000000, 4.543323389463065786E-15, 13.00000000000001066 ) ) ;
#2066=ADVANCED_FACE ( 'NONE', ( #2884 ), #494, .T. ) ;
#2070=CARTESIAN_POINT ( 'NONE',  ( 220.0000000000000000, -20.99999999999999645, 13.00000000000000888 ) ) ;
#2072=PLANE ( 'NONE',  #5922 ) ;
#2078=CARTESIAN_POINT ( 'NONE',  ( 50.01335591787554335, -18.01335591787552559, 12.66922467357069593 ) ) ;
#2080=CARTESIAN_POINT ( 'NONE',  ( 217.0000000000000000, -20.99999999999999645, 13.00000000000000888 ) ) ;
#2083=B_SPLINE_CURVE_WITH_KNOTS ( 'NONE', 3,
 ( #2306, #1834, #602, #4076, #5299, #4806, #4157, #6421, #7144, #1873, #3073, #28 ),
 .UNSPECIFIED., .F., .F.,
 ( 4, 2, 2, 2, 2, 4 ),
 ( 0.000000000000000000, 0.001107519046781883440, 0.002215038093563766880, 0.003322557140345648152, 0.003876316663736585968, 0.004430076187127524219 ),
 .UNSPECIFIED. ) ;
#2092=VECTOR ( 'NONE', #3766, 1000.000000000000000 ) ;
#2093=DIRECTION ( 'NONE',  ( -1.000000000000000000, -0.000000000000000000, -0.000000000000000000 ) ) ;
#2098=CARTESIAN_POINT ( 'NONE',  ( 191.1899843872966471, 6.079033463187697883, 17.21004863381197936 ) ) ;
#2099=FACE_OUTER_BOUND ( 'NONE', #5489, .T. ) ;
#2100=CARTESIAN_POINT ( 'NONE',  ( 186.9059892324150383, -5.031373033403107264, 15.00000000000000888 ) ) ;
#2106=CARTESIAN_POINT ( 'NONE',  ( 217.0000000000000000, 0.000000000000000000, 12.00000000000000711 ) ) ;
#2109=AXIS2_PLACEMENT_3D ( 'NONE', #744, #5448, #3646 ) ;
#2110=ORIENTED_EDGE ( 'NONE', *, *, #4377, .F. ) ;
#2118=LINE ( 'NONE', #3969, #4000 ) ;
#2119=ORIENTED_EDGE ( 'NONE', *, *, #7417, .F. ) ;
#2121=CARTESIAN_POINT ( 'NONE',  ( 189.5040654437683258, 3.000000000000000000, 19.50000000000000711 ) ) ;
#2122=DIRECTION ( 'NONE',  ( 1.000000000000000000, 0.000000000000000000, 0.000000000000000000 ) ) ;
#2125=CYLINDRICAL_SURFACE ( 'NONE', #2706, 2.999999999999999112 ) ;
#2126=DIRECTION ( 'NONE',  ( 1.000000000000000000, 0.000000000000000000, 0.000000000000000000 ) ) ;
#2127=ORIENTED_EDGE ( 'NONE', *, *, #1360, .F. ) ;
#2128=ORIENTED_EDGE ( 'NONE', *, *, #3493, .F. ) ;
#2131=AXIS2_PLACEMENT_3D ( 'NONE', #5342, #7071, #5995 ) ;
#2133=CARTESIAN_POINT ( 'NONE',  ( 188.6381938907515519, 9.028273915299429575, 15.00013323867315940 ) ) ;
#2135=CARTESIAN_POINT ( 'NONE',  ( 209.9999999999999716, -6.000000000000000000, 35.00000000000000000 ) ) ;
#2141=AXIS2_PLACEMENT_3D ( 'NONE', #1432, #3205, #5129 ) ;
#2144=DIRECTION ( 'NONE',  ( 1.000000000000000000, -0.000000000000000000, 0.000000000000000000 ) ) ;
#2150=VECTOR ( 'NONE', #4030, 1000.000000000000000 ) ;
#2157=ORIENTED_EDGE ( 'NONE', *, *, #406, .T. ) ;
#2158=CARTESIAN_POINT ( 'NONE',  ( 52.24271833151664168, -25.80522265072890420, 10.00000000000000888 ) ) ;
#2159=DIRECTION ( 'NONE',  ( 1.000000000000000000, 0.000000000000000000, 0.000000000000000000 ) ) ;
#2161=EDGE_CURVE ( 'NONE', #7239, #4415, #4271, .T. ) ;
#2163=VERTEX_POINT ( 'NONE', #801 ) ;
#2166=ORIENTED_EDGE ( 'NONE', *, *, #483, .T. ) ;
#2169=DIRECTION ( 'NONE',  ( -0.000000000000000000, -1.000000000000000000, -0.000000000000000000 ) ) ;
#2175=AXIS2_PLACEMENT_3D ( 'NONE', #6531, #3723, #3031 ) ;
#2176=CARTESIAN_POINT ( 'NONE',  ( 220.0000000000000000, 18.00000000000000000, 15.00000000000000888 ) ) ;
#2177=CARTESIAN_POINT ( 'NONE',  ( 186.9061174410084334, 9.037698274678149346, 15.00022206379774659 ) ) ;
#2179=DIRECTION ( 'NONE',  ( 0.000000000000000000, 1.000000000000000000, 0.000000000000000000 ) ) ;
#2182=VECTOR ( 'NONE', #6740, 1000.000000000000000 ) ;
#2185=ADVANCED_FACE ( 'NONE', ( #1920 ), #6000, .T. ) ;
#2187=DIRECTION ( 'NONE',  ( 0.000000000000000000, 0.000000000000000000, -1.000000000000000000 ) ) ;
#2191=ORIENTED_EDGE ( 'NONE', *, *, #4675, .F. ) ;
#2192=VERTEX_POINT ( 'NONE', #119 ) ;
#2193=CARTESIAN_POINT ( 'NONE',  ( 185.0000000000000000, 39.99999999999999289, 0.000000000000000000 ) ) ;
#2194=ORIENTED_EDGE ( 'NONE', *, *, #6096, .F. ) ;
#2195=DIRECTION ( 'NONE',  ( 1.000000000000000000, -0.000000000000000000, -0.000000000000000000 ) ) ;
#2196=CARTESIAN_POINT ( 'NONE',  ( 193.5000000000000000, -39.99999999999999289, 10.00000000000000355 ) ) ;
#2201=FACE_OUTER_BOUND ( 'NONE', #5246, .T. ) ;
#2207=DIRECTION ( 'NONE',  ( -0.000000000000000000, 1.000000000000000000, 3.304235192336776498E-16 ) ) ;
#2210=ORIENTED_EDGE ( 'NONE', *, *, #7556, .F. ) ;
#2211=DIRECTION ( 'NONE',  ( 0.000000000000000000, 0.000000000000000000, -1.000000000000000000 ) ) ;
#2212=AXIS2_PLACEMENT_3D ( 'NONE', #64, #711, #3682 ) ;
#2213=EDGE_CURVE ( 'NONE', #2502, #5322, #5612, .T. ) ;
#2215=EDGE_CURVE ( 'NONE', #1645, #2264, #2984, .T. ) ;
#2216=CIRCLE ( 'NONE', #4302, 3.000000000000000000 ) ;
#2220=CARTESIAN_POINT ( 'NONE',  ( 47.00000000000000000, 27.04312195450891565, 12.73853277175702559 ) ) ;
#2223=ORIENTED_EDGE ( 'NONE', *, *, #6269, .F. ) ;
#2225=DIRECTION ( 'NONE',  ( 1.000000000000000000, -0.000000000000000000, -0.000000000000000000 ) ) ;
#2226=LINE ( 'NONE', #5297, #1422 ) ;
#2229=CARTESIAN_POINT ( 'NONE',  ( 217.0000000000000000, 15.08392021690038121, 12.00000000000000711 ) ) ;
#2231=DIRECTION ( 'NONE',  ( -1.000000000000000000, 0.000000000000000000, 0.000000000000000000 ) ) ;
#2233=AXIS2_PLACEMENT_3D ( 'NONE', #4868, #50, #7093 ) ;
#2234=ORIENTED_EDGE ( 'NONE', *, *, #1908, .T. ) ;
#2237=DIRECTION ( 'NONE',  ( 0.000000000000000000, -1.000000000000000000, 0.000000000000000000 ) ) ;
#2238=VERTEX_POINT ( 'NONE', #5962 ) ;
#2247=ORIENTED_EDGE ( 'NONE', *, *, #4075, .T. ) ;
#2250=DIRECTION ( 'NONE',  ( -0.000000000000000000, 0.000000000000000000, -1.000000000000000000 ) ) ;
#2256=CARTESIAN_POINT ( 'NONE',  ( 186.0358176304254698, 8.266324145821753788, 13.49281857405051355 ) ) ;
#2257=DIRECTION ( 'NONE',  ( 1.445602896647337931E-16, -0.000000000000000000, 1.000000000000000000 ) ) ;
#2263=CIRCLE ( 'NONE', #2383, 6.000000000000000000 ) ;
#2264=VERTEX_POINT ( 'NONE', #3385 ) ;
#2265=CARTESIAN_POINT ( 'NONE',  ( 35.00000000000000000, 39.99999999999999289, 10.00000000000000355 ) ) ;
#2267=DIRECTION ( 'NONE',  ( 0.000000000000000000, 0.08715574274766231533, -0.9961946980917453232 ) ) ;
#2269=CARTESIAN_POINT ( 'NONE',  ( 186.9059892324694943, -8.476231918229933271, 15.00000000001430323 ) ) ;
#2275=VECTOR ( 'NONE', #5813, 1000.000000000000000 ) ;
#2280=DIRECTION ( 'NONE',  ( -0.000000000000000000, -0.000000000000000000, 1.000000000000000000 ) ) ;
#2281=VECTOR ( 'NONE', #3930, 1000.000000000000000 ) ;
#2283=ORIENTED_EDGE ( 'NONE', *, *, #271, .T. ) ;
#2285=EDGE_CURVE ( 'NONE', #6005, #6273, #6099, .T. ) ;
#2290=PRODUCT_CONTEXT ( 'NONE', #204, 'mechanical' ) ;
#2291=CARTESIAN_POINT ( 'NONE',  ( 0.000000000000000000, 0.000000000000000000, 35.00000000000000000 ) ) ;
#2292=SPHERICAL_SURFACE ( 'NONE', #2496, 3.000000000000000000 ) ;
#2293=EDGE_LOOP ( 'NONE', ( #1148, #5238, #2694, #351, #4930, #657, #6278 ) ) ;
#2294=EDGE_LOOP ( 'NONE', ( #6663, #4137 ) ) ;
#2303=CARTESIAN_POINT ( 'NONE',  ( 189.5040654437683258, -3.000000000000000888, 19.50000000000000711 ) ) ;
#2304=DIRECTION ( 'NONE',  ( 1.000000000000000000, 0.000000000000000000, 0.000000000000000000 ) ) ;
#2306=CARTESIAN_POINT ( 'NONE',  ( 186.9059892324150383, 5.031373033403108153, 15.00000000000000888 ) ) ;
#2309=CIRCLE ( 'NONE', #579, 3.000000000000001332 ) ;
#2311=ORIENTED_EDGE ( 'NONE', *, *, #3252, .T. ) ;
#2313=CARTESIAN_POINT ( 'NONE',  ( 220.0000000000000000, -9.000000000000001776, 15.00000000000000888 ) ) ;
#2317=EDGE_LOOP ( 'NONE', ( #2333, #6998, #2780, #2558 ) ) ;
#2321=ORIENTED_EDGE ( 'NONE', *, *, #3305, .F. ) ;
#2324=DIRECTION ( 'NONE',  ( 0.000000000000000000, 0.000000000000000000, -1.000000000000000000 ) ) ;
#2326=DIRECTION ( 'NONE',  ( 0.000000000000000000, 0.000000000000000000, -1.000000000000000000 ) ) ;
#2329=DIRECTION ( 'NONE',  ( 0.000000000000000000, 0.000000000000000000, 1.000000000000000000 ) ) ;
#2330=FACE_OUTER_BOUND ( 'NONE', #3816, .T. ) ;
#2331=CARTESIAN_POINT ( 'NONE',  ( 217.0000000000000000, -56.99999999999999289, 7.000000000000000888 ) ) ;
#2333=ORIENTED_EDGE ( 'NONE', *, *, #2526, .T. ) ;
#2336=DIRECTION ( 'NONE',  ( -0.000000000000000000, 1.000000000000000000, -0.000000000000000000 ) ) ;
#2340=AXIS2_PLACEMENT_3D ( 'NONE', #634, #2866, #7558 ) ;
#2342=EDGE_LOOP ( 'NONE', ( #2805, #3556, #6035, #2191 ) ) ;
#2351=ORIENTED_EDGE ( 'NONE', *, *, #5745, .F. ) ;
#2352=ADVANCED_FACE ( 'NONE', ( #4539 ), #2717, .F. ) ;
#2353=EDGE_CURVE ( 'NONE', #6501, #2614, #3225, .T. ) ;
#2355=DIRECTION ( 'NONE',  ( -0.000000000000000000, -0.000000000000000000, 1.000000000000000000 ) ) ;
#2357=ORIENTED_EDGE ( 'NONE', *, *, #7385, .T. ) ;
#2359=FACE_OUTER_BOUND ( 'NONE', #4811, .T. ) ;
#2360=DIRECTION ( 'NONE',  ( 1.000000000000000000, 0.000000000000000000, 0.000000000000000000 ) ) ;
#2361=AXIS2_PLACEMENT_3D ( 'NONE', #5339, #72, #751 ) ;
#2363=EDGE_CURVE ( 'NONE', #1895, #3265, #6760, .T. ) ;
#2364=DIRECTION ( 'NONE',  ( -0.000000000000000000, 0.000000000000000000, 1.000000000000000000 ) ) ;
#2367=CARTESIAN_POINT ( 'NONE',  ( 47.00000000000000000, 30.03170604878415162, 10.00000000000001243 ) ) ;
#2370=CARTESIAN_POINT ( 'NONE',  ( 50.29734716306172970, 18.29734716306171194, 10.98910980934741310 ) ) ;
#2379=EDGE_LOOP ( 'NONE', ( #6438, #895, #6327, #5822 ) ) ;
#2383=AXIS2_PLACEMENT_3D ( 'NONE', #1218, #5420, #1138 ) ;
#2384=VERTEX_POINT ( 'NONE', #3807 ) ;
#2386=CARTESIAN_POINT ( 'NONE',  ( 209.9999999999999716, -6.000000000000000000, 35.00000000000000000 ) ) ;
#2389=CIRCLE ( 'NONE', #6447, 8.500000000000007105 ) ;
#2391=CARTESIAN_POINT ( 'NONE',  ( 50.00000000000000000, 21.91628335801839356, 36.91742634044857141 ) ) ;
#2395=AXIS2_PLACEMENT_3D ( 'NONE', #3388, #5732, #7455 ) ;
#2397=ADVANCED_FACE ( 'NONE', ( #3846 ), #409, .T. ) ;
#2398=DIRECTION ( 'NONE',  ( 0.000000000000000000, 0.000000000000000000, 1.000000000000000000 ) ) ;
#2403=LINE ( 'NONE', #4762, #6111 ) ;
#2405=EDGE_CURVE ( 'NONE', #1231, #2163, #5116, .T. ) ;
#2406=LINE ( 'NONE', #7137, #618 ) ;
#2414=CARTESIAN_POINT ( 'NONE',  ( 220.0000000000000000, 60.00000000000000000, 2.204364238465235507E-14 ) ) ;
#2415=CARTESIAN_POINT ( 'NONE',  ( 3.000000000000000000, 56.99999999999999289, 7.000000000000022204 ) ) ;
#2416=DIRECTION ( 'NONE',  ( 0.000000000000000000, 0.000000000000000000, 1.000000000000000000 ) ) ;
#2417=CIRCLE ( 'NONE', #5009, 8.500000000000007105 ) ;
#2419=ADVANCED_FACE ( 'NONE', ( #3921 ), #7452, .T. ) ;
#2430=EDGE_CURVE ( 'NONE', #6696, #4453, #3650, .T. ) ;
#2436=CYLINDRICAL_SURFACE ( 'NONE', #7018, 6.000000000000015987 ) ;
#2438=ORIENTED_EDGE ( 'NONE', *, *, #5232, .F. ) ;
#2439=EDGE_CURVE ( 'NONE', #6206, #5322, #4879, .T. ) ;
#2443=DIRECTION ( 'NONE',  ( -0.000000000000000000, -1.000000000000000000, -0.000000000000000000 ) ) ;
#2444=CARTESIAN_POINT ( 'NONE',  ( 35.00000000000000000, -39.99999999999999289, 0.000000000000000000 ) ) ;
#2445=FACE_OUTER_BOUND ( 'NONE', #3167, .T. ) ;
#2446=( BOUNDED_CURVE ( )  B_SPLINE_CURVE ( 3, ( #1207, #3563, #4684, #2367 ),
 .UNSPECIFIED., .F., .T. ) 
 B_SPLINE_CURVE_WITH_KNOTS ( ( 4, 4 ),
 ( 4.712388980384689674, 6.283185307179586232 ),
 .UNSPECIFIED. ) 
 CURVE ( )  GEOMETRIC_REPRESENTATION_ITEM ( )  RATIONAL_B_SPLINE_CURVE ( ( 1.000000000000000000, 0.8047378541243649375, 0.8047378541243649375, 1.000000000000000000 ) ) 
 REPRESENTATION_ITEM ( '' )  );
#2449=DIRECTION ( 'NONE',  ( -0.000000000000000000, 1.000000000000000000, 0.000000000000000000 ) ) ;
#2451=CARTESIAN_POINT ( 'NONE',  ( 220.0000000000000000, -56.99999999999999289, 5.510910596163094486E-16 ) ) ;
#2453=FACE_OUTER_BOUND ( 'NONE', #3471, .T. ) ;
#2455=ORIENTED_EDGE ( 'NONE', *, *, #1457, .F. ) ;
#2456=EDGE_LOOP ( 'NONE', ( #5529, #3223, #950, #1622 ) ) ;
#2459=AXIS2_PLACEMENT_3D ( 'NONE', #6528, #5987, #712 ) ;
#2468=EDGE_CURVE ( 'NONE', #647, #7571, #2226, .T. ) ;
#2469=CIRCLE ( 'NONE', #1117, 10.00000000000001954 ) ;
#2470=LINE ( 'NONE', #1276, #4813 ) ;
#2472=ORIENTED_EDGE ( 'NONE', *, *, #4885, .F. ) ;
#2478=DIRECTION ( 'NONE',  ( 0.000000000000000000, 0.9961946980917452121, 0.08715574274766277330 ) ) ;
#2485=FACE_OUTER_BOUND ( 'NONE', #4465, .T. ) ;
#2486=FACE_OUTER_BOUND ( 'NONE', #2896, .T. ) ;
#2488=CARTESIAN_POINT ( 'NONE',  ( 187.4824809480043086, -6.616222357109937668, 15.99851294154436943 ) ) ;
#2492=ORIENTED_EDGE ( 'NONE', *, *, #271, .F. ) ;
#2496=AXIS2_PLACEMENT_3D ( 'NONE', #588, #1783, #6481 ) ;
#2497=CARTESIAN_POINT ( 'NONE',  ( 50.02171387886521359, -28.02758090397744439, 10.00000000000000533 ) ) ;
#2498=ADVANCED_FACE ( 'NONE', ( #4109 ), #7069, .T. ) ;
#2499=CARTESIAN_POINT ( 'NONE',  ( 217.0000000000000000, 3.000000000000000000, 35.00000000000000000 ) ) ;
#2500=ADVANCED_FACE ( 'NONE', ( #524, #1800, #6914 ), #1636, .F. ) ;
#2502=VERTEX_POINT ( 'NONE', #1065 ) ;
#2508=FACE_OUTER_BOUND ( 'NONE', #4004, .T. ) ;
#2511=VECTOR ( 'NONE', #2225, 1000.000000000000000 ) ;
#2513=EDGE_LOOP ( 'NONE', ( #5918, #1184, #4386 ) ) ;
#2514=ADVANCED_FACE ( 'NONE', ( #2872, #5226 ), #7563, .F. ) ;
#2515=EDGE_CURVE ( 'NONE', #2601, #722, #5843, .T. ) ;
#2521=DIRECTION ( 'NONE',  ( -1.000000000000000000, -0.000000000000000000, -0.000000000000000000 ) ) ;
#2522=DIRECTION ( 'NONE',  ( 1.000000000000000000, 0.000000000000000000, 0.000000000000000000 ) ) ;
#2525=VECTOR ( 'NONE', #5994, 1000.000000000000000 ) ;
#2526=EDGE_CURVE ( 'NONE', #4244, #5696, #1367, .T. ) ;
#2527=CARTESIAN_POINT ( 'NONE',  ( 217.0000000000000000, -15.08392021690038121, 12.00000000000000711 ) ) ;
#2529=DIRECTION ( 'NONE',  ( 0.000000000000000000, 0.000000000000000000, 1.000000000000000000 ) ) ;
#2532=EDGE_LOOP ( 'NONE', ( #6594, #4006 ) ) ;
#2536=DIRECTION ( 'NONE',  ( 1.000000000000000000, 0.000000000000000000, 0.000000000000000000 ) ) ;
#2537=DIRECTION ( 'NONE',  ( 1.000000000000000000, 0.000000000000000000, 0.000000000000000000 ) ) ;
#2543=ORIENTED_EDGE ( 'NONE', *, *, #7307, .T. ) ;
#2544=ORIENTED_EDGE ( 'NONE', *, *, #603, .F. ) ;
#2546=DIRECTION ( 'NONE',  ( -0.000000000000000000, 0.03489949670250429292, 0.9993908270190955401 ) ) ;
#2549=FACE_OUTER_BOUND ( 'NONE', #5959, .T. ) ;
#2558=ORIENTED_EDGE ( 'NONE', *, *, #6113, .F. ) ;
#2564=DIRECTION ( 'NONE',  ( 0.000000000000000000, 0.000000000000000000, -1.000000000000000000 ) ) ;
#2565=ADVANCED_FACE ( 'NONE', ( #3725 ), #1872, .T. ) ;
#2566=EDGE_LOOP ( 'NONE', ( #5546, #4779, #538, #7197 ) ) ;
#2567=ORIENTED_EDGE ( 'NONE', *, *, #5163, .T. ) ;
#2569=CARTESIAN_POINT ( 'NONE',  ( 217.0000000000000000, 9.000000000000001776, 18.00000000000001066 ) ) ;
#2570=DIRECTION ( 'NONE',  ( 0.000000000000000000, 0.03489949670250429292, 0.9993908270190955401 ) ) ;
#2572=CARTESIAN_POINT ( 'NONE',  ( 186.9059892324150383, 6.000000000000000000, 18.00000000000001066 ) ) ;
#2574=VERTEX_POINT ( 'NONE', #4915 ) ;
#2588=DIRECTION ( 'NONE',  ( 1.000000000000000000, 0.000000000000000000, 0.000000000000000000 ) ) ;
#2591=ADVANCED_FACE ( 'NONE', ( #1255 ), #3611, .T. ) ;
#2596=CARTESIAN_POINT ( 'NONE',  ( 3.000000000000002665, -28.78532416918554304, 13.00000000000000711 ) ) ;
#2600=DIRECTION ( 'NONE',  ( 1.000000000000000000, 0.000000000000000000, 0.000000000000000000 ) ) ;
#2601=VERTEX_POINT ( 'NONE', #6029 ) ;
#2602=EDGE_LOOP ( 'NONE', ( #3213, #6753, #4625, #1688 ) ) ;
#2603=EDGE_CURVE ( 'NONE', #258, #1604, #1987, .T. ) ;
#2611=TOROIDAL_SURFACE ( 'NONE', #1881, 6.000000000000000000, 3.000000000000000000 ) ;
#2612=LINE ( 'NONE', #2652, #912 ) ;
#2613=DIRECTION ( 'NONE',  ( 0.000000000000000000, 0.9961946980917452121, 0.08715574274766219043 ) ) ;
#2614=VERTEX_POINT ( 'NONE', #3071 ) ;
#2619=AXIS2_PLACEMENT_3D ( 'NONE', #7475, #6242, #395 ) ;
#2622=CARTESIAN_POINT ( 'NONE',  ( 50.02171387886895815, 29.27153168735074829, 10.00000000000000888 ) ) ;
#2626=CIRCLE ( 'NONE', #1278, 3.000000000000000000 ) ;
#2627=DIRECTION ( 'NONE',  ( 1.000000000000000000, 0.000000000000000000, 0.000000000000000000 ) ) ;
#2631=ORIENTED_EDGE ( 'NONE', *, *, #5085, .F. ) ;
#2640=CARTESIAN_POINT ( 'NONE',  ( 186.9464243967159121, -5.771739343384286514, 15.00000000000000888 ) ) ;
#2641=LINE ( 'NONE', #946, #2767 ) ;
#2642=CIRCLE ( 'NONE', #6944, 2.999999999999999112 ) ;
#2643=CIRCLE ( 'NONE', #3636, 3.000000000000000000 ) ;
#2644=CIRCLE ( 'NONE', #4371, 2.999999999999999112 ) ;
#2652=CARTESIAN_POINT ( 'NONE',  ( 220.0000000000000000, 56.99999999999999289, 2.149255132503604690E-14 ) ) ;
#2667=CARTESIAN_POINT ( 'NONE',  ( 203.9378221735088914, 3.000000000000000000, 38.49999999999998579 ) ) ;
#2668=ADVANCED_FACE ( 'NONE', ( #360 ), #6709, .T. ) ;
#2669=ORIENTED_EDGE ( 'NONE', *, *, #3776, .F. ) ;
#2682=CARTESIAN_POINT ( 'NONE',  ( 0.000000000000000000, -28.78532416918554304, 13.00000000000000711 ) ) ;
#2684=DIRECTION ( 'NONE',  ( 1.000000000000000000, 0.000000000000000000, 0.000000000000000000 ) ) ;
#2686=EDGE_CURVE ( 'NONE', #233, #1634, #6898, .T. ) ;
#2687=EDGE_LOOP ( 'NONE', ( #2492, #2438, #1073, #3672 ) ) ;
#2692=CARTESIAN_POINT ( 'NONE',  ( 220.0000000000000000, -28.78532416918554304, 13.00000000000000711 ) ) ;
#2693=APPLICATION_CONTEXT ( 'automotive_design' ) ;
#2694=ORIENTED_EDGE ( 'NONE', *, *, #2215, .F. ) ;
#2695=AXIS2_PLACEMENT_3D ( 'NONE', #1590, #519, #3990 ) ;
#2696=EDGE_CURVE ( 'NONE', #459, #1421, #6775, .T. ) ;
#2703=DIRECTION ( 'NONE',  ( 0.000000000000000000, 0.000000000000000000, 1.000000000000000000 ) ) ;
#2706=AXIS2_PLACEMENT_3D ( 'NONE', #3793, #854, #507 ) ;
#2709=CARTESIAN_POINT ( 'NONE',  ( 187.3640976635304298, 4.216080228656712947, 15.79346707806755745 ) ) ;
#2711=DIRECTION ( 'NONE',  ( 0.000000000000000000, 0.000000000000000000, 1.000000000000000000 ) ) ;
#2712=DIRECTION ( 'NONE',  ( -0.000000000000000000, 0.08715574274766212104, -0.9961946980917452121 ) ) ;
#2715=EDGE_LOOP ( 'NONE', ( #3981, #4050, #326, #7035 ) ) ;
#2717=CYLINDRICAL_SURFACE ( 'NONE', #1546, 2.999999999999999112 ) ;
#2718=DIRECTION ( 'NONE',  ( 0.000000000000000000, 0.08715574274766212104, -0.9961946980917452121 ) ) ;
#2719=ADVANCED_FACE ( 'NONE', ( #4406 ), #1391, .T. ) ;
#2721=ORIENTED_EDGE ( 'NONE', *, *, #4245, .F. ) ;
#2723=AXIS2_PLACEMENT_3D ( 'NONE', #5848, #2951, #4697 ) ;
#2727=DIRECTION ( 'NONE',  ( -0.000000000000000000, -1.000000000000000000, -0.000000000000000000 ) ) ;
#2730=VERTEX_POINT ( 'NONE', #140 ) ;
#2731=CARTESIAN_POINT ( 'NONE',  ( 47.78553976602684372, 30.03170604878551586, 10.00000000000000888 ) ) ;
#2733=EDGE_LOOP ( 'NONE', ( #500, #4088, #1774, #3184 ) ) ;
#2734=LINE ( 'NONE', #6744, #3353 ) ;
#2737=ORIENTED_EDGE ( 'NONE', *, *, #3912, .F. ) ;
#2740=CARTESIAN_POINT ( 'NONE',  ( 201.3397459621555754, 6.000000000000000000, 39.99999999999997868 ) ) ;
#2741=CIRCLE ( 'NONE', #3984, 13.99999999999999112 ) ;
#2751=AXIS2_PLACEMENT_3D ( 'NONE', #2569, #1955, #4962 ) ;
#2755=CARTESIAN_POINT ( 'NONE',  ( 217.0000000000000000, -15.08392021690038121, 15.00000000000000888 ) ) ;
#2757=CIRCLE ( 'NONE', #7064, 3.000000000000002665 ) ;
#2759=CARTESIAN_POINT ( 'NONE',  ( 217.0000000000000000, -56.99999999999999289, 7.000000000000000888 ) ) ;
#2761=AXIS2_PLACEMENT_3D ( 'NONE', #1562, #3344, #990 ) ;
#2763=ADVANCED_FACE ( 'NONE', ( #3680 ), #779, .T. ) ;
#2767=VECTOR ( 'NONE', #4492, 1000.000000000000000 ) ;
#2775=EDGE_CURVE ( 'NONE', #5563, #2574, #7391, .T. ) ;
#2778=CYLINDRICAL_SURFACE ( 'NONE', #5463, 3.000000000000000000 ) ;
#2780=ORIENTED_EDGE ( 'NONE', *, *, #1317, .F. ) ;
#2781=LINE ( 'NONE', #6783, #4711 ) ;
#2782=LINE ( 'NONE', #4095, #4561 ) ;
#2783=( BOUNDED_CURVE ( )  B_SPLINE_CURVE ( 3, ( #2121, #5595, #319, #7320 ),
 .UNSPECIFIED., .F., .T. ) 
 B_SPLINE_CURVE_WITH_KNOTS ( ( 4, 4 ),
 ( 1.570796326794896114, 2.418858405776376230 ),
 .UNSPECIFIED. ) 
 CURVE ( )  GEOMETRIC_REPRESENTATION_ITEM ( )  RATIONAL_B_SPLINE_CURVE ( ( 1.000000000000000000, 0.9409585518440986007, 0.9409585518440986007, 1.000000000000000000 ) ) 
 REPRESENTATION_ITEM ( '' )  );
#2785=ORIENTED_EDGE ( 'NONE', *, *, #5085, .T. ) ;
#2786=VERTEX_POINT ( 'NONE', #2013 ) ;
#2787=AXIS2_PLACEMENT_3D ( 'NONE', #4297, #4730, #1797 ) ;
#2788=CARTESIAN_POINT ( 'NONE',  ( 50.00000000000000000, 17.91234734164656928, 13.00000000000000711 ) ) ;
#2789=CARTESIAN_POINT ( 'NONE',  ( 176.5000000000000000, -39.99999999999999289, 0.000000000000000000 ) ) ;
#2791=CARTESIAN_POINT ( 'NONE',  ( 209.9999999999999716, 6.000000000000000000, 35.00000000000000000 ) ) ;
#2795=VERTEX_POINT ( 'NONE', #4520 ) ;
#2798=DIRECTION ( 'NONE',  ( 0.000000000000000000, 0.000000000000000000, -1.000000000000000000 ) ) ;
#2801=FACE_OUTER_BOUND ( 'NONE', #4525, .T. ) ;
#2802=EDGE_CURVE ( 'NONE', #2795, #3147, #6782, .T. ) ;
#2805=ORIENTED_EDGE ( 'NONE', *, *, #7397, .T. ) ;
#2806=CARTESIAN_POINT ( 'NONE',  ( 220.0000000000000000, -60.00000000000000000, 0.000000000000000000 ) ) ;
#2807=EDGE_CURVE ( 'NONE', #3862, #5693, #2781, .T. ) ;
#2811=LINE ( 'NONE', #3856, #2281 ) ;
#2812=ORIENTED_EDGE ( 'NONE', *, *, #6304, .F. ) ;
#2813=DIRECTION ( 'NONE',  ( -0.000000000000000000, -0.000000000000000000, -1.000000000000000000 ) ) ;
#2821=VERTEX_POINT ( 'NONE', #3937 ) ;
#2822=ORIENTED_EDGE ( 'NONE', *, *, #5881, .F. ) ;
#2823=CARTESIAN_POINT ( 'NONE',  ( 50.04196010845020481, 18.04196010845019060, 12.50000000000000711 ) ) ;
#2826=CARTESIAN_POINT ( 'NONE',  ( 189.9621738748845132, 6.608040114328683323, 16.14673353903353004 ) ) ;
#2828=EDGE_CURVE ( 'NONE', #7091, #1634, #2734, .T. ) ;
#2835=DIRECTION ( 'NONE',  ( 1.000000000000000000, 0.000000000000000000, 0.000000000000000000 ) ) ;
#2836=LINE ( 'NONE', #843, #5346 ) ;
#2837=DIRECTION ( 'NONE',  ( 0.000000000000000000, 0.08715574274766287044, -0.9961946980917452121 ) ) ;
#2838=VECTOR ( 'NONE', #2195, 1000.000000000000000 ) ;
#2839=CARTESIAN_POINT ( 'NONE',  ( 186.9059892324149814, -9.000000000000000000, 14.99999999999999289 ) ) ;
#2840=ORIENTED_EDGE ( 'NONE', *, *, #2215, .T. ) ;
#2845=AXIS2_PLACEMENT_3D ( 'NONE', #1435, #2521, #4874 ) ;
#2846=CARTESIAN_POINT ( 'NONE',  ( 3.000000000000002665, -56.99999999999999289, 10.00000000000000000 ) ) ;
#2848=CARTESIAN_POINT ( 'NONE',  ( 47.00000000000000000, 0.000000000000000000, 35.00000000000000000 ) ) ;
#2849=DIRECTION ( 'NONE',  ( 1.000000000000000000, 0.000000000000000000, 0.000000000000000000 ) ) ;
#2852=ORIENTED_EDGE ( 'NONE', *, *, #2828, .F. ) ;
#2856=DIRECTION ( 'NONE',  ( 0.000000000000000000, 0.000000000000000000, -1.000000000000000000 ) ) ;
#2857=CARTESIAN_POINT ( 'NONE',  ( 185.0000000000000000, -39.99999999999999289, 0.000000000000000000 ) ) ;
#2861=CARTESIAN_POINT ( 'NONE',  ( 193.5000000000000000, 39.99999999999999289, 10.00000000000000355 ) ) ;
#2862=DIRECTION ( 'NONE',  ( -0.000000000000000000, 0.000000000000000000, 1.000000000000000000 ) ) ;
#2864=DIRECTION ( 'NONE',  ( 0.000000000000000000, 0.000000000000000000, -1.000000000000000000 ) ) ;
#2866=DIRECTION ( 'NONE',  ( 0.000000000000000000, 1.000000000000000000, 0.000000000000000000 ) ) ;
#2867=CARTESIAN_POINT ( 'NONE',  ( 220.0000000000000000, -60.00000000000000000, 10.00000000000000000 ) ) ;
#2871=ORIENTED_EDGE ( 'NONE', *, *, #4452, .F. ) ;
#2872=FACE_BOUND ( 'NONE', #3752, .T. ) ;
#2875=DIRECTION ( 'NONE',  ( -0.000000000000000000, -1.000000000000000000, -0.000000000000000000 ) ) ;
#2878=AXIS2_PLACEMENT_3D ( 'NONE', #2596, #6102, #1443 ) ;
#2884=FACE_OUTER_BOUND ( 'NONE', #3427, .T. ) ;
#2885=DIRECTION ( 'NONE',  ( -1.000000000000000000, -0.000000000000000000, -0.000000000000000000 ) ) ;
#2887=CARTESIAN_POINT ( 'NONE',  ( 49.39900052591036683, -24.62867772107294329, 12.93565788627303803 ) ) ;
#2888=DIRECTION ( 'NONE',  ( 0.000000000000000000, 0.000000000000000000, -1.000000000000000000 ) ) ;
#2889=AXIS2_PLACEMENT_3D ( 'NONE', #6773, #3357, #2159 ) ;
#2890=CIRCLE ( 'NONE', #3638, 3.000000000000001332 ) ;
#2891=EDGE_LOOP ( 'NONE', ( #4941, #5172, #5148 ) ) ;
#2893=CARTESIAN_POINT ( 'NONE',  ( 50.00000000000000000, 24.00878702352406791, 10.00000000000000888 ) ) ;
#2896=EDGE_LOOP ( 'NONE', ( #1155, #1455, #1005, #3898 ) ) ;
#2898=EDGE_CURVE ( 'NONE', #2730, #5749, #3599, .T. ) ;
#2899=LINE ( 'NONE', #5248, #4313 ) ;
#2906=DIRECTION ( 'NONE',  ( -0.000000000000000000, -0.000000000000000000, 1.000000000000000000 ) ) ;
#2909=VECTOR ( 'NONE', #4996, 1000.000000000000000 ) ;
#2910=ORIENTED_EDGE ( 'NONE', *, *, #3963, .T. ) ;
#2914=CARTESIAN_POINT ( 'NONE',  ( 187.3752131572541373, -4.201998947814849394, 15.81271967794823574 ) ) ;
#2915=AXIS2_PLACEMENT_3D ( 'NONE', #4600, #5253, #2326 ) ;
#2919=VERTEX_POINT ( 'NONE', #4422 ) ;
#2923=CARTESIAN_POINT ( 'NONE',  ( 49.94932960940505495, -23.57319494935126514, 10.00000000000205702 ) ) ;
#2928=CARTESIAN_POINT ( 'NONE',  ( 217.0000000000000000, 60.00000000000000000, 2.204364238465235507E-14 ) ) ;
#2937=DIRECTION ( 'NONE',  ( -0.4999999999999960032, -0.000000000000000000, -0.8660254037844411501 ) ) ;
#2946=ORIENTED_EDGE ( 'NONE', *, *, #492, .T. ) ;
#2951=DIRECTION ( 'NONE',  ( 0.000000000000000000, 1.000000000000000000, 0.000000000000000000 ) ) ;
#2952=AXIS2_PLACEMENT_3D ( 'NONE', #2135, #3840, #2711 ) ;
#2954=ORIENTED_EDGE ( 'NONE', *, *, #6096, .T. ) ;
#2956=EDGE_CURVE ( 'NONE', #5312, #6714, #4213, .T. ) ;
#2963=CARTESIAN_POINT ( 'NONE',  ( 220.0000000000000000, 20.99999999999999645, 13.00000000000000888 ) ) ;
#2964=AXIS2_PLACEMENT_3D ( 'NONE', #3236, #1459, #1966 ) ;
#2965=ORIENTED_EDGE ( 'NONE', *, *, #1452, .F. ) ;
#2969=DIRECTION ( 'NONE',  ( 0.000000000000000000, 0.000000000000000000, -1.000000000000000000 ) ) ;
#2973=CYLINDRICAL_SURFACE ( 'NONE', #2233, 13.99999999999999112 ) ;
#2974=FACE_OUTER_BOUND ( 'NONE', #7115, .T. ) ;
#2976=VERTEX_POINT ( 'NONE', #1373 ) ;
#2981=CARTESIAN_POINT ( 'NONE',  ( 3.000000000000002665, 0.000000000000000000, 35.00000000000000000 ) ) ;
#2982=DIRECTION ( 'NONE',  ( 0.000000000000000000, 0.000000000000000000, -1.000000000000000000 ) ) ;
#2984=( BOUNDED_CURVE ( )  B_SPLINE_CURVE ( 3, ( #5535, #6071, #4198, #6543 ),
 .UNSPECIFIED., .F., .T. ) 
 B_SPLINE_CURVE_WITH_KNOTS ( ( 4, 4 ),
 ( 3.141592653589793116, 4.712388980384689674 ),
 .UNSPECIFIED. ) 
 CURVE ( )  GEOMETRIC_REPRESENTATION_ITEM ( )  RATIONAL_B_SPLINE_CURVE ( ( 1.000000000000000000, 0.8047378541243649375, 0.8047378541243649375, 1.000000000000000000 ) ) 
 REPRESENTATION_ITEM ( '' )  );
#2989=DIRECTION ( 'NONE',  ( -0.8660254037844413721, 0.000000000000000000, 0.4999999999999950595 ) ) ;
#3008=AXIS2_PLACEMENT_3D ( 'NONE', #4218, #172, #244 ) ;
#3013=ORIENTED_EDGE ( 'NONE', *, *, #4411, .T. ) ;
#3016=CYLINDRICAL_SURFACE ( 'NONE', #5169, 3.000000000000000888 ) ;
#3020=ADVANCED_FACE ( 'NONE', ( #5008 ), #2072, .F. ) ;
#3021=ORIENTED_EDGE ( 'NONE', *, *, #5199, .T. ) ;
#3026=DIRECTION ( 'NONE',  ( -0.000000000000000000, -0.000000000000000000, 1.000000000000000000 ) ) ;
#3028=DIRECTION ( 'NONE',  ( 0.000000000000000000, 0.000000000000000000, 1.000000000000000000 ) ) ;
#3030=VECTOR ( 'NONE', #6038, 1000.000000000000000 ) ;
#3031=DIRECTION ( 'NONE',  ( 0.000000000000000000, 0.000000000000000000, 1.000000000000000000 ) ) ;
#3034=DIRECTION ( 'NONE',  ( 1.000000000000000000, 0.000000000000000000, 0.000000000000000000 ) ) ;
#3039=ORIENTED_EDGE ( 'NONE', *, *, #1908, .F. ) ;
#3045=EDGE_LOOP ( 'NONE', ( #739, #1693, #3703, #4071 ) ) ;
#3046=PRODUCT ( 'base', 'base', '', ( #2290 ) ) ;
#3048=CARTESIAN_POINT ( 'NONE',  ( 47.81196995442319064, -25.80454930986227424, 9.999999999997962519 ) ) ;
#3049=CARTESIAN_POINT ( 'NONE',  ( 217.0000000000000000, 20.99999999999999645, 7.000000000000009770 ) ) ;
#3050=ORIENTED_EDGE ( 'NONE', *, *, #5562, .F. ) ;
#3054=CARTESIAN_POINT ( 'NONE',  ( 50.00000000000000000, -22.78166690339260825, 13.00000000000000711 ) ) ;
#3056=ORIENTED_EDGE ( 'NONE', *, *, #2898, .F. ) ;
#3059=ORIENTED_EDGE ( 'NONE', *, *, #3135, .T. ) ;
#3066=LINE ( 'NONE', #1249, #5412 ) ;
#3067=CARTESIAN_POINT ( 'NONE',  ( 50.04196010845020481, 18.04196010845019060, 12.50000000000000711 ) ) ;
#3071=CARTESIAN_POINT ( 'NONE',  ( 217.0000000000000000, -60.00000000000000000, 3.000000000000000444 ) ) ;
#3073=CARTESIAN_POINT ( 'NONE',  ( 188.5076150991777411, 8.869380270722979631, 15.00000000000000533 ) ) ;
#3074=CARTESIAN_POINT ( 'NONE',  ( 189.2293793704153018, -5.809691905097411180, 19.02422976478239391 ) ) ;
#3076=ORIENTED_EDGE ( 'NONE', *, *, #4645, .T. ) ;
#3079=DIRECTION ( 'NONE',  ( -1.000000000000000000, 0.000000000000000000, 0.000000000000000000 ) ) ;
#3088=DIRECTION ( 'NONE',  ( 0.000000000000000000, -1.000000000000000000, -2.065146995210484941E-16 ) ) ;
#3090=ORIENTED_EDGE ( 'NONE', *, *, #1788, .T. ) ;
#3091=DIRECTION ( 'NONE',  ( 0.000000000000000000, 1.000000000000000000, 0.000000000000000000 ) ) ;
#3094=DIRECTION ( 'NONE',  ( -1.000000000000000000, -0.000000000000000000, -0.000000000000000000 ) ) ;
#3095=DIRECTION ( 'NONE',  ( -0.000000000000000000, -1.000000000000000000, -1.836970198721029934E-16 ) ) ;
#3099=FACE_OUTER_BOUND ( 'NONE', #4200, .T. ) ;
#3101=EDGE_CURVE ( 'NONE', #5579, #1932, #4504, .T. ) ;
#3102=VECTOR ( 'NONE', #4659, 1000.000000000000114 ) ;
#3109=ORIENTED_EDGE ( 'NONE', *, *, #6184, .T. ) ;
#3114=CIRCLE ( 'NONE', #1015, 2.999999999999999112 ) ;
#3117=ORIENTED_EDGE ( 'NONE', *, *, #2285, .F. ) ;
#3119=VECTOR ( 'NONE', #4750, 1000.000000000000000 ) ;
#3120=VECTOR ( 'NONE', #6381, 1000.000000000000000 ) ;
#3124=DIRECTION ( 'NONE',  ( 0.000000000000000000, 0.000000000000000000, -1.000000000000000000 ) ) ;
#3125=VECTOR ( 'NONE', #2355, 1000.000000000000000 ) ;
#3129=CIRCLE ( 'NONE', #5344, 3.000000000000000000 ) ;
#3133=AXIS2_PLACEMENT_3D ( 'NONE', #5298, #6460, #601 ) ;
#3134=ORIENTED_EDGE ( 'NONE', *, *, #2956, .F. ) ;
#3135=EDGE_CURVE ( 'NONE', #5312, #6160, #3346, .T. ) ;
#3138=DIRECTION ( 'NONE',  ( 0.000000000000000000, 0.000000000000000000, -1.000000000000000000 ) ) ;
#3139=CIRCLE ( 'NONE', #7072, 13.99999999999999112 ) ;
#3141=ORIENTED_EDGE ( 'NONE', *, *, #1037, .F. ) ;
#3143=DIRECTION ( 'NONE',  ( 0.000000000000000000, 0.000000000000000000, -1.000000000000000000 ) ) ;
#3146=ORIENTED_EDGE ( 'NONE', *, *, #4523, .T. ) ;
#3147=VERTEX_POINT ( 'NONE', #5691 ) ;
#3149=CARTESIAN_POINT ( 'NONE',  ( 3.000000000000002665, 27.04312195450891565, 12.73853277175702559 ) ) ;
#3151=EDGE_CURVE ( 'NONE', #3744, #5755, #6842, .T. ) ;
#3158=CIRCLE ( 'NONE', #6966, 3.000000000000000444 ) ;
#3164=DIRECTION ( 'NONE',  ( 1.000000000000000000, 0.000000000000000000, 0.000000000000000000 ) ) ;
#3167=EDGE_LOOP ( 'NONE', ( #4980, #2852, #4599, #2737 ) ) ;
#3169=DIRECTION ( 'NONE',  ( -1.000000000000000000, 0.000000000000000000, 0.000000000000000000 ) ) ;
#3170=ORIENTED_EDGE ( 'NONE', *, *, #6654, .F. ) ;
#3175=ADVANCED_FACE ( 'NONE', ( #412 ), #672, .T. ) ;
#3181=EDGE_LOOP ( 'NONE', ( #7210, #297, #4462 ) ) ;
#3182=CARTESIAN_POINT ( 'NONE',  ( 0.000000000000000000, 24.95512646718981742, 2.183290662734949983 ) ) ;
#3184=ORIENTED_EDGE ( 'NONE', *, *, #5294, .F. ) ;
#3186=CARTESIAN_POINT ( 'NONE',  ( 43.50000000000001421, 39.99999999999999289, 10.00000000000000355 ) ) ;
#3191=ORIENTED_EDGE ( 'NONE', *, *, #7105, .F. ) ;
#3192=CIRCLE ( 'NONE', #4188, 8.500000000000007105 ) ;
#3193=AXIS2_PLACEMENT_3D ( 'NONE', #6058, #782, #3138 ) ;
#3196=ORIENTED_EDGE ( 'NONE', *, *, #4452, .T. ) ;
#3197=DIRECTION ( 'NONE',  ( 0.000000000000000000, 0.1666666666666668239, -0.9860132971832694659 ) ) ;
#3198=DIRECTION ( 'NONE',  ( 0.000000000000000000, 0.000000000000000000, -1.000000000000000000 ) ) ;
#3200=EDGE_CURVE ( 'NONE', #5898, #3265, #1489, .T. ) ;
#3204=CARTESIAN_POINT ( 'NONE',  ( 47.00000000000000000, 27.28271252673189551, 10.00000000000000711 ) ) ;
#3205=DIRECTION ( 'NONE',  ( -0.000000000000000000, -0.000000000000000000, 1.000000000000000000 ) ) ;
#3208=LINE ( 'NONE', #354, #4690 ) ;
#3209=CARTESIAN_POINT ( 'NONE',  ( 217.0000000000000000, -60.00000000000000000, 7.000000000000000888 ) ) ;
#3212=VECTOR ( 'NONE', #7383, 1000.000000000000000 ) ;
#3213=ORIENTED_EDGE ( 'NONE', *, *, #3151, .T. ) ;
#3214=DIRECTION ( 'NONE',  ( 0.000000000000000000, 0.9961946980917452121, 0.08715574274766277330 ) ) ;
#3220=CYLINDRICAL_SURFACE ( 'NONE', #1232, 8.500000000000007105 ) ;
#3223=ORIENTED_EDGE ( 'NONE', *, *, #971, .F. ) ;
#3225=LINE ( 'NONE', #4961, #5980 ) ;
#3227=CARTESIAN_POINT ( 'NONE',  ( 3.000000000000002665, 21.91628335801839356, 36.91742634044857141 ) ) ;
#3230=ORIENTED_EDGE ( 'NONE', *, *, #3899, .T. ) ;
#3231=ORIENTED_EDGE ( 'NONE', *, *, #4350, .F. ) ;
#3235=ORIENTED_EDGE ( 'NONE', *, *, #5594, .T. ) ;
#3236=CARTESIAN_POINT ( 'NONE',  ( 3.000000000000002665, -28.78532416918554304, 13.00000000000000711 ) ) ;
#3239=ORIENTED_EDGE ( 'NONE', *, *, #6101, .F. ) ;
#3240=CIRCLE ( 'NONE', #6309, 13.99999999999999112 ) ;
#3241=AXIS2_PLACEMENT_3D ( 'NONE', #4724, #2443, #2329 ) ;
#3244=PLANE ( 'NONE',  #1524 ) ;
#3245=ORIENTED_EDGE ( 'NONE', *, *, #585, .T. ) ;
#3251=CARTESIAN_POINT ( 'NONE',  ( 0.000000000000000000, 56.99999999999999289, 3.000000000000021760 ) ) ;
#3252=EDGE_CURVE ( 'NONE', #5749, #2730, #1969, .T. ) ;
#3255=AXIS2_PLACEMENT_3D ( 'NONE', #495, #1036, #1113 ) ;
#3257=CARTESIAN_POINT ( 'NONE',  ( 0.000000000000000000, -28.78532416918554304, 10.00000000000000711 ) ) ;
#3258=CARTESIAN_POINT ( 'NONE',  ( 47.00000000000000000, 24.90486745229362953, 37.17889356869155648 ) ) ;
#3263=CIRCLE ( 'NONE', #678, 22.00000000000000355 ) ;
#3265=VERTEX_POINT ( 'NONE', #4193 ) ;
#3267=CARTESIAN_POINT ( 'NONE',  ( 220.0000000000000000, 20.99999999999999645, 13.00000000000000888 ) ) ;
#3276=ORIENTED_EDGE ( 'NONE', *, *, #6748, .F. ) ;
#3279=( BOUNDED_CURVE ( )  B_SPLINE_CURVE ( 3, ( #6126, #1387, #7241, #7133 ),
 .UNSPECIFIED., .F., .T. ) 
 B_SPLINE_CURVE_WITH_KNOTS ( ( 4, 4 ),
 ( 0.000000000000000000, 1.570796326794896558 ),
 .UNSPECIFIED. ) 
 CURVE ( )  GEOMETRIC_REPRESENTATION_ITEM ( )  RATIONAL_B_SPLINE_CURVE ( ( 1.000000000000000000, 0.8047378541243649375, 0.8047378541243649375, 1.000000000000000000 ) ) 
 REPRESENTATION_ITEM ( '' )  );
#3282=ADVANCED_FACE ( 'NONE', ( #2453 ), #7368, .T. ) ;
#3283=FACE_BOUND ( 'NONE', #7249, .T. ) ;
#3286=ORIENTED_EDGE ( 'NONE', *, *, #1566, .F. ) ;
#3290=CARTESIAN_POINT ( 'NONE',  ( 3.000000000000002665, 60.00000000000000000, 10.00000000000002309 ) ) ;
#3291=EDGE_LOOP ( 'NONE', ( #4164, #4593, #7086 ) ) ;
#3294=FACE_OUTER_BOUND ( 'NONE', #41, .T. ) ;
#3297=DIRECTION ( 'NONE',  ( 0.000000000000000000, 0.000000000000000000, 1.000000000000000000 ) ) ;
#3302=ORIENTED_EDGE ( 'NONE', *, *, #5881, .T. ) ;
#3305=EDGE_CURVE ( 'NONE', #2919, #5270, #7335, .T. ) ;
#3309=ORIENTED_EDGE ( 'NONE', *, *, #3857, .F. ) ;
#3313=CARTESIAN_POINT ( 'NONE',  ( 209.9999999999999716, -3.000000000000000888, 35.00000000000000000 ) ) ;
#3314=EDGE_CURVE ( 'NONE', #5020, #5359, #4309, .T. ) ;
#3315=CARTESIAN_POINT ( 'NONE',  ( 3.000000000000002665, 0.000000000000000000, 35.00000000000000000 ) ) ;
#3317=AXIS2_PLACEMENT_3D ( 'NONE', #4992, #4260, #3760 ) ;
#3318=FACE_OUTER_BOUND ( 'NONE', #2317, .T. ) ;
#3322=EDGE_CURVE ( 'NONE', #3547, #4957, #4383, .T. ) ;
#3324=CARTESIAN_POINT ( 'NONE',  ( 217.0000000000000000, -9.000000000000001776, 15.00000000000000888 ) ) ;
#3325=( BOUNDED_CURVE ( )  B_SPLINE_CURVE ( 3, ( #4755, #4170, #6513, #3054 ),
 .UNSPECIFIED., .F., .T. ) 
 B_SPLINE_CURVE_WITH_KNOTS ( ( 4, 4 ),
 ( 3.141592653589793116, 4.712388980384689674 ),
 .UNSPECIFIED. ) 
 CURVE ( )  GEOMETRIC_REPRESENTATION_ITEM ( )  RATIONAL_B_SPLINE_CURVE ( ( 1.000000000000000000, 0.8047378541243649375, 0.8047378541243649375, 1.000000000000000000 ) ) 
 REPRESENTATION_ITEM ( '' )  );
#3326=DIRECTION ( 'NONE',  ( 0.000000000000000000, 1.156482317317871725E-15, -1.000000000000000000 ) ) ;
#3327=ORIENTED_EDGE ( 'NONE', *, *, #1317, .T. ) ;
#3328=ORIENTED_EDGE ( 'NONE', *, *, #4523, .F. ) ;
#3332=CARTESIAN_POINT ( 'NONE',  ( 188.5919081759386415, 3.158066926375936223, 17.92009726762579191 ) ) ;
#3337=CIRCLE ( 'NONE', #14, 3.000000000000002665 ) ;
#3342=DIRECTION ( 'NONE',  ( -1.000000000000000000, -0.000000000000000000, -0.000000000000000000 ) ) ;
#3344=DIRECTION ( 'NONE',  ( -1.000000000000000000, 0.000000000000000000, 0.000000000000000000 ) ) ;
#3345=DIRECTION ( 'NONE',  ( 0.000000000000000000, -0.1666666666666668239, -0.9860132971832694659 ) ) ;
#3346=LINE ( 'NONE', #4079, #5807 ) ;
#3351=ORIENTED_EDGE ( 'NONE', *, *, #2828, .T. ) ;
#3353=VECTOR ( 'NONE', #3829, 1000.000000000000000 ) ;
#3356=CARTESIAN_POINT ( 'NONE',  ( 188.6380400399839061, -9.000000000000001776, 15.00000000000000888 ) ) ;
#3357=DIRECTION ( 'NONE',  ( 0.000000000000000000, 0.000000000000000000, 1.000000000000000000 ) ) ;
#3360=ORIENTED_EDGE ( 'NONE', *, *, #5531, .F. ) ;
#3363=FACE_OUTER_BOUND ( 'NONE', #1491, .T. ) ;
#3365=VERTEX_POINT ( 'NONE', #1366 ) ;
#3370=VECTOR ( 'NONE', #4054, 1000.000000000000000 ) ;
#3373=CARTESIAN_POINT ( 'NONE',  ( 220.0000000000000000, 60.00000000000000000, 3.000000000000021760 ) ) ;
#3375=DIRECTION ( 'NONE',  ( 1.000000000000000000, 0.000000000000000000, 0.000000000000000000 ) ) ;
#3377=DIRECTION ( 'NONE',  ( -0.000000000000000000, -1.000000000000000000, -3.304235192336776498E-16 ) ) ;
#3382=EDGE_CURVE ( 'NONE', #584, #7026, #754, .T. ) ;
#3383=ORIENTED_EDGE ( 'NONE', *, *, #7556, .T. ) ;
#3385=CARTESIAN_POINT ( 'NONE',  ( 53.00000000000000711, -22.78166690339260825, 10.00000000000000711 ) ) ;
#3387=DIRECTION ( 'NONE',  ( -0.000000000000000000, -0.000000000000000000, 1.000000000000000000 ) ) ;
#3388=CARTESIAN_POINT ( 'NONE',  ( 35.00000000000000000, 39.99999999999999289, 0.000000000000000000 ) ) ;
#3390=CIRCLE ( 'NONE', #3133, 6.000000000000000000 ) ;
#3405=FACE_BOUND ( 'NONE', #7158, .T. ) ;
#3416=LINE ( 'NONE', #6863, #5619 ) ;
#3419=CARTESIAN_POINT ( 'NONE',  ( 217.0000000000000000, 56.99999999999999289, 3.000000000000021760 ) ) ;
#3425=UNCERTAINTY_MEASURE_WITH_UNIT (LENGTH_MEASURE( 1.000000000000000082E-05 ), #632, 'distance_accuracy_value', 'NONE');
#3427=EDGE_LOOP ( 'NONE', ( #7486, #5862, #5851 ) ) ;
#3428=DIRECTION ( 'NONE',  ( 0.000000000000000000, 1.000000000000000000, 0.000000000000000000 ) ) ;
#3429=CARTESIAN_POINT ( 'NONE',  ( 0.000000000000000000, 30.03170604878415162, 7.000000000000013323 ) ) ;
#3430=FACE_OUTER_BOUND ( 'NONE', #168, .T. ) ;
#3432=ORIENTED_EDGE ( 'NONE', *, *, #2363, .T. ) ;
#3433=ORIENTED_EDGE ( 'NONE', *, *, #2439, .T. ) ;
#3435=DIRECTION ( 'NONE',  ( -1.000000000000000000, -0.000000000000000000, 0.000000000000000000 ) ) ;
#3438=FACE_OUTER_BOUND ( 'NONE', #5251, .T. ) ;
#3440=ORIENTED_EDGE ( 'NONE', *, *, #7397, .F. ) ;
#3447=EDGE_CURVE ( 'NONE', #5693, #4453, #2641, .T. ) ;
#3450=DIRECTION ( 'NONE',  ( 1.000000000000000000, -0.000000000000000000, -0.000000000000000000 ) ) ;
#3454=CARTESIAN_POINT ( 'NONE',  ( 191.6458868871019661, 6.000000000000000888, 17.60487178029247346 ) ) ;
#3457=CARTESIAN_POINT ( 'NONE',  ( 47.00000000000000000, 27.28271252673189196, 10.00000000000001421 ) ) ;
#3460=DIRECTION ( 'NONE',  ( 0.000000000000000000, 0.000000000000000000, 1.000000000000000000 ) ) ;
#3463=AXIS2_PLACEMENT_3D ( 'NONE', #3674, #735, #4283 ) ;
#3468=LINE ( 'NONE', #2313, #4610 ) ;
#3470=CARTESIAN_POINT ( 'NONE',  ( 3.000000000000002665, -24.98477067547739239, 35.87248741756260983 ) ) ;
#3471=EDGE_LOOP ( 'NONE', ( #1260, #6182, #1909 ) ) ;
#3474=ADVANCED_FACE ( 'NONE', ( #1514 ), #3878, .T. ) ;
#3479=DIRECTION ( 'NONE',  ( 0.000000000000000000, 1.000000000000000000, -0.000000000000000000 ) ) ;
#3482=FACE_OUTER_BOUND ( 'NONE', #6244, .T. ) ;
#3486=( NAMED_UNIT ( * ) PLANE_ANGLE_UNIT ( ) SI_UNIT ( $, .RADIAN. ) );
#3491=CIRCLE ( 'NONE', #3616, 3.000000000000000888 ) ;
#3492=VERTEX_POINT ( 'NONE', #5680 ) ;
#3493=EDGE_CURVE ( 'NONE', #6371, #3543, #4607, .T. ) ;
#3495=DIRECTION ( 'NONE',  ( 0.000000000000000000, 0.000000000000000000, -1.000000000000000000 ) ) ;
#3496=DIRECTION ( 'NONE',  ( 0.000000000000000000, 0.000000000000000000, -1.000000000000000000 ) ) ;
#3499=AXIS2_PLACEMENT_3D ( 'NONE', #46, #1312, #660 ) ;
#3504=CIRCLE ( 'NONE', #4241, 8.500000000000007105 ) ;
#3508=ORIENTED_EDGE ( 'NONE', *, *, #984, .F. ) ;
#3511=ADVANCED_FACE ( 'NONE', ( #7519 ), #5798, .F. ) ;
#3522=DIRECTION ( 'NONE',  ( 0.000000000000000000, 0.000000000000000000, -1.000000000000000000 ) ) ;
#3524=VERTEX_POINT ( 'NONE', #5064 ) ;
#3526=AXIS2_PLACEMENT_3D ( 'NONE', #2106, #6141, #5574 ) ;
#3527=SHAPE_REPRESENTATION_RELATIONSHIP ( 'NONE' , 'NONE' ,  #915, #4741 ) ;
#3530=FACE_OUTER_BOUND ( 'NONE', #4454, .T. ) ;
#3532=ORIENTED_EDGE ( 'NONE', *, *, #3931, .T. ) ;
#3535=CARTESIAN_POINT ( 'NONE',  ( 187.5739056480075533, -3.719611233821797480, 16.15686516701557807 ) ) ;
#3536=CARTESIAN_POINT ( 'NONE',  ( 217.0000000000000000, -15.08392021690038121, 12.00000000000000711 ) ) ;
#3537=DIRECTION ( 'NONE',  ( 0.000000000000000000, -1.000000000000000000, 0.000000000000000000 ) ) ;
#3543=VERTEX_POINT ( 'NONE', #2220 ) ;
#3547=VERTEX_POINT ( 'NONE', #6292 ) ;
#3552=ORIENTED_EDGE ( 'NONE', *, *, #984, .T. ) ;
#3556=ORIENTED_EDGE ( 'NONE', *, *, #3575, .F. ) ;
#3558=DIRECTION ( 'NONE',  ( -1.000000000000000000, 0.000000000000000000, 0.000000000000000000 ) ) ;
#3559=CARTESIAN_POINT ( 'NONE',  ( 47.00000000000000000, 0.000000000000000000, 60.00000000000000711 ) ) ;
#3561=DIRECTION ( 'NONE',  ( 0.8660254037844400399, 0.000000000000000000, -0.4999999999999976685 ) ) ;
#3563=CARTESIAN_POINT ( 'NONE',  ( 53.00000000000000000, 27.53693130344647955, 10.00000000000001066 ) ) ;
#3572=DIRECTION ( 'NONE',  ( 0.000000000000000000, 1.000000000000000000, 2.065146995210484941E-16 ) ) ;
#3575=EDGE_CURVE ( 'NONE', #3524, #5445, #1993, .T. ) ;
#3581=VECTOR ( 'NONE', #2169, 1000.000000000000000 ) ;
#3582=CARTESIAN_POINT ( 'NONE',  ( 26.49999999999999645, -39.99999999999999289, 10.00000000000000355 ) ) ;
#3584=ADVANCED_FACE ( 'NONE', ( #2445 ), #7103, .T. ) ;
#3588=CARTESIAN_POINT ( 'NONE',  ( 47.39276988301253368, -25.78715168812822611, 12.89530150989326707 ) ) ;
#3589=DIRECTION ( 'NONE',  ( 0.000000000000000000, 0.000000000000000000, -1.000000000000000000 ) ) ;
#3592=ORIENTED_EDGE ( 'NONE', *, *, #1642, .T. ) ;
#3597=DIRECTION ( 'NONE',  ( 0.000000000000000000, 0.000000000000000000, 1.000000000000000000 ) ) ;
#3599=CIRCLE ( 'NONE', #6295, 8.500000000000007105 ) ;
#3601=DIRECTION ( 'NONE',  ( 0.000000000000000000, -0.9993908270190955401, 0.03489949670250346025 ) ) ;
#3606=DIRECTION ( 'NONE',  ( 0.000000000000000000, -1.000000000000000000, -3.304235192336776498E-16 ) ) ;
#3607=ADVANCED_FACE ( 'NONE', ( #3530 ), #635, .T. ) ;
#3611=CYLINDRICAL_SURFACE ( 'NONE', #23, 3.000000000000002665 ) ;
#3614=CARTESIAN_POINT ( 'NONE',  ( 191.6486100594302684, -6.000000000000000888, 17.60723011670769722 ) ) ;
#3615=ADVANCED_FACE ( 'NONE', ( #6413 ), #5781, .T. ) ;
#3616=AXIS2_PLACEMENT_3D ( 'NONE', #2415, #4111, #6461 ) ;
#3621=DIRECTION ( 'NONE',  ( 0.000000000000000000, 0.000000000000000000, 1.000000000000000000 ) ) ;
#3623=ORIENTED_EDGE ( 'NONE', *, *, #5632, .F. ) ;
#3630=EDGE_CURVE ( 'NONE', #6935, #6160, #2216, .T. ) ;
#3632=ORIENTED_EDGE ( 'NONE', *, *, #6304, .T. ) ;
#3633=LINE ( 'NONE', #5932, #3125 ) ;
#3635=AXIS2_PLACEMENT_3D ( 'NONE', #4619, #3345, #5648 ) ;
#3636=AXIS2_PLACEMENT_3D ( 'NONE', #536, #2280, #6471 ) ;
#3638=AXIS2_PLACEMENT_3D ( 'NONE', #5061, #3913, #5719 ) ;
#3641=EDGE_CURVE ( 'NONE', #5055, #2919, #626, .T. ) ;
#3646=DIRECTION ( 'NONE',  ( 0.000000000000000000, 0.000000000000000000, 1.000000000000000000 ) ) ;
#3647=DIRECTION ( 'NONE',  ( 1.000000000000000000, 0.000000000000000000, 0.000000000000000000 ) ) ;
#3648=CARTESIAN_POINT ( 'NONE',  ( 53.00000000000000711, 20.99999999999999645, 10.00000000000001066 ) ) ;
#3650=CIRCLE ( 'NONE', #567, 25.00000000000000000 ) ;
#3651=DIRECTION ( 'NONE',  ( 0.000000000000000000, 0.000000000000000000, 1.000000000000000000 ) ) ;
#3652=CARTESIAN_POINT ( 'NONE',  ( 49.73397419454932589, 25.59482593276749895, 10.00000000000000178 ) ) ;
#3656=LINE ( 'NONE', #6498, #1022 ) ;
#3657=CARTESIAN_POINT ( 'NONE',  ( 187.2689031676866307, -7.021191553082208436, 15.62858537466729025 ) ) ;
#3662=CIRCLE ( 'NONE', #334, 3.000000000000000000 ) ;
#3663=DIRECTION ( 'NONE',  ( -1.000000000000000000, 0.000000000000000000, 0.000000000000000000 ) ) ;
#3669=ORIENTED_EDGE ( 'NONE', *, *, #831, .T. ) ;
#3672=ORIENTED_EDGE ( 'NONE', *, *, #6864, .T. ) ;
#3674=CARTESIAN_POINT ( 'NONE',  ( 50.00000000000000000, 0.000000000000000000, 35.00000000000000000 ) ) ;
#3677=LINE ( 'NONE', #5982, #5744 ) ;
#3678=CARTESIAN_POINT ( 'NONE',  ( 217.0000000000000000, -56.99999999999999289, 3.000000000000000000 ) ) ;
#3680=FACE_OUTER_BOUND ( 'NONE', #1516, .T. ) ;
#3682=DIRECTION ( 'NONE',  ( 0.000000000000000000, 0.000000000000000000, -1.000000000000000000 ) ) ;
#3697=AXIS2_PLACEMENT_3D ( 'NONE', #684, #2416, #4776 ) ;
#3699=CARTESIAN_POINT ( 'NONE',  ( 48.55648163125127326, -25.48496883304055061, 10.00000000000205169 ) ) ;
#3702=EDGE_CURVE ( 'NONE', #5020, #7224, #1711, .T. ) ;
#3703=ORIENTED_EDGE ( 'NONE', *, *, #3797, .F. ) ;
#3709=FACE_OUTER_BOUND ( 'NONE', #654, .T. ) ;
#3718=ORIENTED_EDGE ( 'NONE', *, *, #3305, .T. ) ;
#3720=EDGE_CURVE ( 'NONE', #6371, #3, #4726, .T. ) ;
#3722=PRODUCT_DEFINITION_SHAPE ( 'NONE', 'NONE',  #1644 ) ;
#3723=DIRECTION ( 'NONE',  ( 0.000000000000000000, 1.000000000000000000, 0.000000000000000000 ) ) ;
#3725=FACE_OUTER_BOUND ( 'NONE', #1823, .T. ) ;
#3730=ADVANCED_FACE ( 'NONE', ( #4408 ), #217, .F. ) ;
#3734=DIRECTION ( 'NONE',  ( 0.000000000000000000, 0.000000000000000000, 1.000000000000000000 ) ) ;
#3744=VERTEX_POINT ( 'NONE', #3209 ) ;
#3746=LINE ( 'NONE', #6231, #381 ) ;
#3749=TOROIDAL_SURFACE ( 'NONE', #4858, 22.00000000000000355, 3.000000000000000000 ) ;
#3752=EDGE_LOOP ( 'NONE', ( #923, #3230 ) ) ;
#3753=DIRECTION ( 'NONE',  ( 0.000000000000000000, -1.836970198721029934E-16, 1.000000000000000000 ) ) ;
#3754=CIRCLE ( 'NONE', #427, 3.000000000000002665 ) ;
#3757=ORIENTED_EDGE ( 'NONE', *, *, #6132, .T. ) ;
#3759=DIRECTION ( 'NONE',  ( 0.000000000000000000, 0.000000000000000000, 1.000000000000000000 ) ) ;
#3760=DIRECTION ( 'NONE',  ( 0.000000000000000000, 0.000000000000000000, 1.000000000000000000 ) ) ;
#3761=AXIS2_PLACEMENT_3D ( 'NONE', #2499, #727, #1883 ) ;
#3763=DIRECTION ( 'NONE',  ( 0.000000000000000000, -1.000000000000000000, -0.000000000000000000 ) ) ;
#3766=DIRECTION ( 'NONE',  ( -0.000000000000000000, 0.08715574274766212104, -0.9961946980917452121 ) ) ;
#3769=VERTEX_POINT ( 'NONE', #1437 ) ;
#3775=DIRECTION ( 'NONE',  ( -1.000000000000000000, 0.000000000000000000, 0.000000000000000000 ) ) ;
#3776=EDGE_CURVE ( 'NONE', #4453, #3147, #175, .T. ) ;
#3778=EDGE_LOOP ( 'NONE', ( #758, #1319, #4719, #5507 ) ) ;
#3780=CIRCLE ( 'NONE', #6716, 3.000000000000002665 ) ;
#3782=ORIENTED_EDGE ( 'NONE', *, *, #2898, .T. ) ;
#3785=CIRCLE ( 'NONE', #2915, 2.999999999999999112 ) ;
#3789=CARTESIAN_POINT ( 'NONE',  ( 3.000000000000002665, -60.00000000000000000, 3.000000000000000000 ) ) ;
#3793=CARTESIAN_POINT ( 'NONE',  ( 53.00000000000000711, 4.543323389463065786E-15, 13.00000000000001066 ) ) ;
#3796=EDGE_LOOP ( 'NONE', ( #4405, #1280, #5296, #7405 ) ) ;
#3797=EDGE_CURVE ( 'NONE', #1310, #2601, #976, .T. ) ;
#3802=CARTESIAN_POINT ( 'NONE',  ( 187.5208673656504175, -7.524439173533908232, 15.00000000000001066 ) ) ;
#3807=CARTESIAN_POINT ( 'NONE',  ( 50.00000000000000000, 15.08392021690038121, 15.00000000000000888 ) ) ;
#3808=DIRECTION ( 'NONE',  ( 0.000000000000000000, -0.08715574274766212104, 0.9961946980917452121 ) ) ;
#3814=EDGE_CURVE ( 'NONE', #5579, #3936, #4952, .T. ) ;
#3815=DIRECTION ( 'NONE',  ( -1.000000000000000000, -0.000000000000000000, -0.000000000000000000 ) ) ;
#3816=EDGE_LOOP ( 'NONE', ( #2050, #6079, #1038, #5282 ) ) ;
#3818=DIRECTION ( 'NONE',  ( 1.000000000000000000, 0.000000000000000000, 0.000000000000000000 ) ) ;
#3821=ORIENTED_EDGE ( 'NONE', *, *, #5058, .T. ) ;
#3824=AXIS2_PLACEMENT_3D ( 'NONE', #2386, #4749, #6041 ) ;
#3826=CARTESIAN_POINT ( 'NONE',  ( 185.0000000000000000, 39.99999999999999289, 10.00000000000000355 ) ) ;
#3827=ORIENTED_EDGE ( 'NONE', *, *, #1839, .T. ) ;
#3829=DIRECTION ( 'NONE',  ( -0.000000000000000000, 1.000000000000000000, 3.304235192336776498E-16 ) ) ;
#3835=AXIS2_PLACEMENT_3D ( 'NONE', #2053, #5486, #2588 ) ;
#3840=DIRECTION ( 'NONE',  ( 0.000000000000000000, 1.000000000000000000, 0.000000000000000000 ) ) ;
#3845=ORIENTED_EDGE ( 'NONE', *, *, #327, .T. ) ;
#3846=FACE_OUTER_BOUND ( 'NONE', #4357, .T. ) ;
#3855=LINE ( 'NONE', #5080, #1731 ) ;
#3856=CARTESIAN_POINT ( 'NONE',  ( 220.0000000000000000, 56.99999999999999289, 10.00000000000002132 ) ) ;
#3857=EDGE_CURVE ( 'NONE', #4957, #7205, #6019, .T. ) ;
#3858=EDGE_LOOP ( 'NONE', ( #2127, #6912 ) ) ;
#3859=CIRCLE ( 'NONE', #533, 3.000000000000000000 ) ;
#3861=CARTESIAN_POINT ( 'NONE',  ( 48.51085693943250021, 26.66014758463033729, 12.77153349490077794 ) ) ;
#3862=VERTEX_POINT ( 'NONE', #1050 ) ;
#3866=LINE ( 'NONE', #891, #493 ) ;
#3874=CARTESIAN_POINT ( 'NONE',  ( 217.0000000000000000, -3.000000000000000000, 35.00000000000000000 ) ) ;
#3875=CARTESIAN_POINT ( 'NONE',  ( 189.0640241484130968, 7.505526787993156645, 15.36891305950205577 ) ) ;
#3878=CYLINDRICAL_SURFACE ( 'NONE', #2695, 3.000000000000007994 ) ;
#3880=CIRCLE ( 'NONE', #2761, 3.000000000000000888 ) ;
#3882=ORIENTED_EDGE ( 'NONE', *, *, #219, .F. ) ;
#3885=DIRECTION ( 'NONE',  ( 0.000000000000000000, 0.000000000000000000, 1.000000000000000000 ) ) ;
#3887=ADVANCED_FACE ( 'NONE', ( #1545 ), #5134, .T. ) ;
#3888=DIRECTION ( 'NONE',  ( 0.000000000000000000, -0.9961946980917452121, -0.08715574274766212104 ) ) ;
#3892=VERTEX_POINT ( 'NONE', #6282 ) ;
#3898=ORIENTED_EDGE ( 'NONE', *, *, #4810, .T. ) ;
#3899=EDGE_CURVE ( 'NONE', #3492, #1345, #3240, .T. ) ;
#3901=CARTESIAN_POINT ( 'NONE',  ( 51.79800105182918912, 27.71015215774388096, 10.00000000000000888 ) ) ;
#3902=FACE_OUTER_BOUND ( 'NONE', #3796, .T. ) ;
#3904=AXIS2_PLACEMENT_3D ( 'NONE', #2740, #3561, #5869 ) ;
#3907=CARTESIAN_POINT ( 'NONE',  ( 209.9999999999999716, 6.000000000000000000, 41.00000000000002132 ) ) ;
#3909=ORIENTED_EDGE ( 'NONE', *, *, #2430, .F. ) ;
#3911=DIRECTION ( 'NONE',  ( -1.007940753403772230E-16, 0.08715574274766275942, -0.9961946980917452121 ) ) ;
#3912=EDGE_CURVE ( 'NONE', #131, #4590, #7510, .T. ) ;
#3913=DIRECTION ( 'NONE',  ( 4.036065081973857683E-17, 0.03489949670250346025, 0.9993908270190956511 ) ) ;
#3919=EDGE_LOOP ( 'NONE', ( #5432, #3932, #5147, #2965 ) ) ;
#3921=FACE_OUTER_BOUND ( 'NONE', #3919, .T. ) ;
#3923=DIRECTION ( 'NONE',  ( 0.000000000000000000, 1.000000000000000000, 0.000000000000000000 ) ) ;
#3928=ORIENTED_EDGE ( 'NONE', *, *, #928, .T. ) ;
#3929=DIRECTION ( 'NONE',  ( 0.000000000000000000, 0.000000000000000000, 1.000000000000000000 ) ) ;
#3930=DIRECTION ( 'NONE',  ( -1.000000000000000000, 0.000000000000000000, 0.000000000000000000 ) ) ;
#3931=EDGE_CURVE ( 'NONE', #4614, #7465, #6941, .T. ) ;
#3932=ORIENTED_EDGE ( 'NONE', *, *, #6758, .F. ) ;
#3933=AXIS2_PLACEMENT_3D ( 'NONE', #2867, #6251, #7559 ) ;
#3934=CARTESIAN_POINT ( 'NONE',  ( 53.00000000000002132, -18.00000000000000000, 10.00000000000000888 ) ) ;
#3936=VERTEX_POINT ( 'NONE', #5631 ) ;
#3937=CARTESIAN_POINT ( 'NONE',  ( 203.9378221735088630, -6.000000000000000000, 38.50000000000000000 ) ) ;
#3938=TOROIDAL_SURFACE ( 'NONE', #2212, 6.000000000000000000, 3.000000000000000000 ) ;
#3940=AXIS2_PLACEMENT_3D ( 'NONE', #6722, #2600, #2564 ) ;
#3942=EDGE_CURVE ( 'NONE', #529, #2192, #1632, .T. ) ;
#3945=TOROIDAL_SURFACE ( 'NONE', #4433, 22.00000000000000355, 3.000000000000000000 ) ;
#3950=ORIENTED_EDGE ( 'NONE', *, *, #1521, .T. ) ;
#3959=CARTESIAN_POINT ( 'NONE',  ( 185.0000000000000000, 39.99999999999999289, 0.000000000000000000 ) ) ;
#3963=EDGE_CURVE ( 'NONE', #6542, #4415, #5940, .T. ) ;
#3964=ORIENTED_EDGE ( 'NONE', *, *, #4949, .T. ) ;
#3966=LINE ( 'NONE', #4083, #2275 ) ;
#3968=DIRECTION ( 'NONE',  ( 0.000000000000000000, -0.08715574274766212104, 0.9961946980917452121 ) ) ;
#3969=CARTESIAN_POINT ( 'NONE',  ( 50.00000000000000000, -22.89008536370704050, 9.895301509892497904 ) ) ;
#3971=VECTOR ( 'NONE', #4177, 1000.000000000000000 ) ;
#3974=FACE_OUTER_BOUND ( 'NONE', #4886, .T. ) ;
#3978=DIRECTION ( 'NONE',  ( -0.000000000000000000, 1.000000000000000000, 3.304235192336776498E-16 ) ) ;
#3980=VECTOR ( 'NONE', #5710, 1000.000000000000000 ) ;
#3981=ORIENTED_EDGE ( 'NONE', *, *, #5594, .F. ) ;
#3983=CARTESIAN_POINT ( 'NONE',  ( 0.000000000000000000, 56.99999999999999289, 7.000000000000022204 ) ) ;
#3984=AXIS2_PLACEMENT_3D ( 'NONE', #767, #1887, #2969 ) ;
#3987=CARTESIAN_POINT ( 'NONE',  ( 186.4659479370544375, 6.011053575986605502, 14.23782611900703010 ) ) ;
#3990=DIRECTION ( 'NONE',  ( -0.8660254037844404840, 0.000000000000000000, 0.4999999999999968359 ) ) ;
#3992=CIRCLE ( 'NONE', #1285, 3.000000000000002665 ) ;
#3993=VERTEX_POINT ( 'NONE', #5096 ) ;
#3995=CARTESIAN_POINT ( 'NONE',  ( 209.9999999999999716, 6.000000000000000000, 35.00000000000000000 ) ) ;
#3996=DIRECTION ( 'NONE',  ( 0.000000000000000000, 2.065146995210484941E-16, -1.000000000000000000 ) ) ;
#3997=AXIS2_PLACEMENT_3D ( 'NONE', #991, #5152, #7490 ) ;
#3999=DIRECTION ( 'NONE',  ( -1.000000000000000000, 0.000000000000000000, 0.000000000000000000 ) ) ;
#4000=VECTOR ( 'NONE', #5016, 1000.000000000000114 ) ;
#4001=EDGE_CURVE ( 'NONE', #570, #6714, #6404, .T. ) ;
#4004=EDGE_LOOP ( 'NONE', ( #3196, #35, #2544, #1031 ) ) ;
#4006=ORIENTED_EDGE ( 'NONE', *, *, #6203, .T. ) ;
#4009=ADVANCED_FACE ( 'NONE', ( #1822 ), #2611, .T. ) ;
#4011=CARTESIAN_POINT ( 'NONE',  ( 188.6380400399839061, -7.242640687119284770, 15.00000000000001066 ) ) ;
#4012=EDGE_LOOP ( 'NONE', ( #1988, #6911, #5474, #7522 ) ) ;
#4029=CARTESIAN_POINT ( 'NONE',  ( 176.5000000000000000, -39.99999999999999289, 10.00000000000000355 ) ) ;
#4030=DIRECTION ( 'NONE',  ( -1.000000000000000000, 0.000000000000000000, 0.000000000000000000 ) ) ;
#4038=DIRECTION ( 'NONE',  ( 1.000000000000000000, 0.000000000000000000, 0.000000000000000000 ) ) ;
#4039=CARTESIAN_POINT ( 'NONE',  ( 217.0000000000000000, -5.510910596163110263E-16, 3.000000000000011102 ) ) ;
#4043=EDGE_CURVE ( 'NONE', #6224, #3543, #3114, .T. ) ;
#4046=DIRECTION ( 'NONE',  ( 0.000000000000000000, 0.000000000000000000, 1.000000000000000000 ) ) ;
#4047=ORIENTED_EDGE ( 'NONE', *, *, #1878, .F. ) ;
#4049=DIRECTION ( 'NONE',  ( 0.000000000000000000, 0.000000000000000000, -1.000000000000000000 ) ) ;
#4050=ORIENTED_EDGE ( 'NONE', *, *, #909, .T. ) ;
#4054=DIRECTION ( 'NONE',  ( -0.000000000000000000, -1.000000000000000000, -2.065146995210484941E-16 ) ) ;
#4057=DIRECTION ( 'NONE',  ( 1.000000000000000000, 0.000000000000000000, 0.000000000000000000 ) ) ;
#4059=AXIS2_PLACEMENT_3D ( 'NONE', #1828, #3606, #4186 ) ;
#4063=CIRCLE ( 'NONE', #2340, 2.999999999999999112 ) ;
#4064=CARTESIAN_POINT ( 'NONE',  ( 217.0000000000000000, -3.000000000000000888, 18.00000000000001066 ) ) ;
#4067=DIRECTION ( 'NONE',  ( 0.000000000000000000, 0.000000000000000000, -1.000000000000000000 ) ) ;
#4071=ORIENTED_EDGE ( 'NONE', *, *, #5323, .F. ) ;
#4075=EDGE_CURVE ( 'NONE', #7239, #7538, #528, .T. ) ;
#4076=CARTESIAN_POINT ( 'NONE',  ( 187.1032342689625523, 6.494950219283388115, 15.00000000000001066 ) ) ;
#4077=AXIS2_PLACEMENT_3D ( 'NONE', #6772, #3197, #881 ) ;
#4078=ADVANCED_FACE ( 'NONE', ( #1277 ), #2292, .T. ) ;
#4079=CARTESIAN_POINT ( 'NONE',  ( 220.0000000000000000, -60.00000000000000000, 7.000000000000000000 ) ) ;
#4081=ORIENTED_EDGE ( 'NONE', *, *, #941, .T. ) ;
#4083=CARTESIAN_POINT ( 'NONE',  ( 193.5000000000000000, 39.99999999999999289, 0.000000000000000000 ) ) ;
#4088=ORIENTED_EDGE ( 'NONE', *, *, #865, .F. ) ;
#4090=SPHERICAL_SURFACE ( 'NONE', #4737, 3.000000000000000000 ) ;
#4091=VERTEX_POINT ( 'NONE', #3559 ) ;
#4095=CARTESIAN_POINT ( 'NONE',  ( 201.3397459621555754, -3.000000000000000888, 39.99999999999997868 ) ) ;
#4101=CARTESIAN_POINT ( 'NONE',  ( 217.0000000000000000, -1.445602896647342072E-15, 7.000000000000012434 ) ) ;
#4102=EDGE_CURVE ( 'NONE', #7468, #4738, #4463, .T. ) ;
#4103=CARTESIAN_POINT ( 'NONE',  ( 209.9999999999999716, 9.000000000000001776, 18.00000000000001066 ) ) ;
#4107=ORIENTED_EDGE ( 'NONE', *, *, #5786, .T. ) ;
#4109=FACE_OUTER_BOUND ( 'NONE', #3291, .T. ) ;
#4111=DIRECTION ( 'NONE',  ( -0.000000000000000000, -1.000000000000000000, 0.000000000000000000 ) ) ;
#4114=VECTOR ( 'NONE', #6300, 1000.000000000000000 ) ;
#4115=( BOUNDED_SURFACE ( )  B_SPLINE_SURFACE ( 3, 2, ( 
 ( #477, #6374, #7399 ),
 ( #3454, #6248, #7365 ),
 ( #2098, #6905, #3332 ),
 ( #400, #5757, #6867 ),
 ( #2826, #5178, #2709 ),
 ( #5794, #1587, #4447 ),
 ( #3875, #7444, #3987 ),
 ( #516, #943, #1016 ),
 ( #445, #6791, #2256 ),
 ( #2133, #2177, #1511 ) ),
 .UNSPECIFIED., .F., .F., .T. ) 
 B_SPLINE_SURFACE_WITH_KNOTS ( ( 4, 2, 2, 2, 4 ),
 ( 3, 3 ),
 ( 1.570796326794896558, 1.965851602983812896, 2.360906879172729234, 2.755962155361645571, 3.151017431550562353 ),
 ( 0.000000000000000000, 1.000000000000000000 ),
 .UNSPECIFIED. ) 
 GEOMETRIC_REPRESENTATION_ITEM ( )  RATIONAL_B_SPLINE_SURFACE ( (
 ( 1.000000000000000000, 0.7071067811865475727, 1.000000000000000000),
 ( 1.000000000000000000, 0.7304008256110219310, 1.000000000000000000),
 ( 1.000000000000000000, 0.7524735362752019707, 1.000000000000000000),
 ( 1.000000000000000000, 0.7918254010917817887, 1.000000000000000000),
 ( 1.000000000000000000, 0.8090963605090051303, 1.000000000000000000),
 ( 1.000000000000000000, 0.8372423287799937164, 1.000000000000000000),
 ( 1.000000000000000000, 0.8481212422410200347, 1.000000000000000000),
 ( 1.000000000000000000, 0.8625983312438976203, 1.000000000000000000),
 ( 1.000000000000000000, 0.8662073891937924763, 1.000000000000000000),
 ( 1.000000000000000000, 0.8660189933120610029, 1.000000000000000000) ) ) 
 REPRESENTATION_ITEM ( '' )  SURFACE ( )  );
#4123=CARTESIAN_POINT ( 'NONE',  ( 50.00000000000000000, 30.03170604878415162, 13.00000000000001066 ) ) ;
#4124=ORIENTED_EDGE ( 'NONE', *, *, #4852, .F. ) ;
#4128=ORIENTED_EDGE ( 'NONE', *, *, #656, .F. ) ;
#4131=LINE ( 'NONE', #5435, #6446 ) ;
#4133=ORIENTED_EDGE ( 'NONE', *, *, #5871, .F. ) ;
#4136=DIRECTION ( 'NONE',  ( 0.000000000000000000, 0.000000000000000000, 1.000000000000000000 ) ) ;
#4137=ORIENTED_EDGE ( 'NONE', *, *, #3200, .T. ) ;
#4138=ADVANCED_FACE ( 'NONE', ( #2974 ), #4678, .F. ) ;
#4147=CARTESIAN_POINT ( 'NONE',  ( 50.00000000000000000, 24.90486745229362953, 37.17889356869155648 ) ) ;
#4156=CARTESIAN_POINT ( 'NONE',  ( 50.00000000000000000, 0.000000000000000000, 35.00000000000000000 ) ) ;
#4157=CARTESIAN_POINT ( 'NONE',  ( 187.7042917662940340, 7.845594361310616272, 15.00000000000000888 ) ) ;
#4158=CARTESIAN_POINT ( 'NONE',  ( 189.5040654437683258, -6.000000000000000000, 19.50000000000000355 ) ) ;
#4164=ORIENTED_EDGE ( 'NONE', *, *, #983, .T. ) ;
#4166=CARTESIAN_POINT ( 'NONE',  ( 46.99999999999999289, -25.88825784476432545, 10.00000000000000533 ) ) ;
#4167=DIRECTION ( 'NONE',  ( 1.000000000000000000, 0.000000000000000000, 0.000000000000000000 ) ) ;
#4169=EDGE_LOOP ( 'NONE', ( #1952, #2157, #4483, #6885 ) ) ;
#4170=CARTESIAN_POINT ( 'NONE',  ( 48.75735931288071612, -25.78715168812825809, 12.89530150989249258 ) ) ;
#4172=ORIENTED_EDGE ( 'NONE', *, *, #5713, .F. ) ;
#4175=FACE_OUTER_BOUND ( 'NONE', #650, .T. ) ;
#4176=ADVANCED_FACE ( 'NONE', ( #6123 ), #2044, .T. ) ;
#4177=DIRECTION ( 'NONE',  ( 0.000000000000000000, -1.000000000000000000, 0.000000000000000000 ) ) ;
#4185=FACE_OUTER_BOUND ( 'NONE', #1183, .T. ) ;
#4186=DIRECTION ( 'NONE',  ( 0.000000000000000000, 0.000000000000000000, -1.000000000000000000 ) ) ;
#4188=AXIS2_PLACEMENT_3D ( 'NONE', #781, #3759, #3647 ) ;
#4189=VECTOR ( 'NONE', #5292, 1000.000000000000000 ) ;
#4191=CARTESIAN_POINT ( 'NONE',  ( 0.000000000000000000, -28.78532416918554304, 7.000000000000006217 ) ) ;
#4193=CARTESIAN_POINT ( 'NONE',  ( 209.9999999999999716, -6.000000000000000000, 28.99999999999998579 ) ) ;
#4196=ORIENTED_EDGE ( 'NONE', *, *, #5004, .F. ) ;
#4198=CARTESIAN_POINT ( 'NONE',  ( 53.00000000000000000, -26.29852790585433198, 10.00000000000000888 ) ) ;
#4200=EDGE_LOOP ( 'NONE', ( #5919, #3909, #2110, #2351, #3276 ) ) ;
#4202=CARTESIAN_POINT ( 'NONE',  ( 48.57048730951588311, -28.62906503896529031, 10.00000000000000533 ) ) ;
#4203=ADVANCED_FACE ( 'NONE', ( #6737 ), #1967, .T. ) ;
#4210=ORIENTED_EDGE ( 'NONE', *, *, #3493, .T. ) ;
#4213=CIRCLE ( 'NONE', #5313, 6.000000000000000000 ) ;
#4216=ADVANCED_FACE ( 'NONE', ( #3709 ), #5402, .F. ) ;
#4217=FACE_OUTER_BOUND ( 'NONE', #4169, .T. ) ;
#4218=CARTESIAN_POINT ( 'NONE',  ( 185.0000000000000000, -39.99999999999999289, 0.000000000000000000 ) ) ;
#4221=DIRECTION ( 'NONE',  ( -0.000000000000000000, -0.000000000000000000, 1.000000000000000000 ) ) ;
#4222=CYLINDRICAL_SURFACE ( 'NONE', #1428, 2.999999999999999112 ) ;
#4224=CARTESIAN_POINT ( 'NONE',  ( 48.96690339724148799, 26.58792303940015600, 10.00000000000068745 ) ) ;
#4226=CARTESIAN_POINT ( 'NONE',  ( 50.00000000000000000, -21.98659819442010388, 35.76778892745510063 ) ) ;
#4240=ORIENTED_EDGE ( 'NONE', *, *, #911, .T. ) ;
#4241=AXIS2_PLACEMENT_3D ( 'NONE', #2193, #4046, #5237 ) ;
#4244=VERTEX_POINT ( 'NONE', #240 ) ;
#4245=EDGE_CURVE ( 'NONE', #6726, #7349, #4469, .T. ) ;
#4248=EDGE_LOOP ( 'NONE', ( #6659, #2567, #7535, #2543 ) ) ;
#4254=ORIENTED_EDGE ( 'NONE', *, *, #7454, .T. ) ;
#4260=DIRECTION ( 'NONE',  ( -1.000000000000000000, 0.000000000000000000, 0.000000000000000000 ) ) ;
#4264=CARTESIAN_POINT ( 'NONE',  ( 3.000000000000002665, 30.03170604878415162, 7.000000000000012434 ) ) ;
#4266=CARTESIAN_POINT ( 'NONE',  ( 191.1954203846383393, -6.078081970536771017, 17.21475634561434731 ) ) ;
#4271=LINE ( 'NONE', #4780, #3030 ) ;
#4272=AXIS2_PLACEMENT_3D ( 'NONE', #2176, #2211, #6902 ) ;
#4278=ORIENTED_EDGE ( 'NONE', *, *, #5690, .T. ) ;
#4279=ORIENTED_EDGE ( 'NONE', *, *, #2696, .F. ) ;
#4283=DIRECTION ( 'NONE',  ( 0.000000000000000000, 0.000000000000000000, -1.000000000000000000 ) ) ;
#4284=DIRECTION ( 'NONE',  ( 0.000000000000000000, 0.000000000000000000, -1.000000000000000000 ) ) ;
#4286=EDGE_CURVE ( 'NONE', #4738, #131, #2811, .T. ) ;
#4293=CYLINDRICAL_SURFACE ( 'NONE', #1225, 8.500000000000007105 ) ;
#4294=DIRECTION ( 'NONE',  ( 0.000000000000000000, -0.03489949670250429292, -0.9993908270190955401 ) ) ;
#4297=CARTESIAN_POINT ( 'NONE',  ( 185.0000000000000000, -39.99999999999999289, 10.00000000000000355 ) ) ;
#4302=AXIS2_PLACEMENT_3D ( 'NONE', #2331, #5376, #2982 ) ;
#4306=DIRECTION ( 'NONE',  ( 0.000000000000000000, 0.000000000000000000, -1.000000000000000000 ) ) ;
#4308=CIRCLE ( 'NONE', #1348, 6.000000000000019540 ) ;
#4309=CIRCLE ( 'NONE', #1721, 3.000000000000000000 ) ;
#4310=DIRECTION ( 'NONE',  ( 1.000000000000000000, 0.000000000000000000, 0.000000000000000000 ) ) ;
#4313=VECTOR ( 'NONE', #4677, 1000.000000000000000 ) ;
#4314=ORIENTED_EDGE ( 'NONE', *, *, #5268, .F. ) ;
#4315=EDGE_CURVE ( 'NONE', #7201, #3547, #2118, .T. ) ;
#4319=VECTOR ( 'NONE', #5697, 1000.000000000000000 ) ;
#4321=CARTESIAN_POINT ( 'NONE',  ( 217.0000000000000000, 56.99999999999999289, 0.000000000000000000 ) ) ;
#4332=AXIS2_PLACEMENT_3D ( 'NONE', #5559, #1356, #2478 ) ;
#4342=ORIENTED_EDGE ( 'NONE', *, *, #1625, .T. ) ;
#4349=CYLINDRICAL_SURFACE ( 'NONE', #3761, 3.000000000000002665 ) ;
#4350=EDGE_CURVE ( 'NONE', #3892, #1997, #5110, .T. ) ;
#4351=ORIENTED_EDGE ( 'NONE', *, *, #80, .T. ) ;
#4352=ORIENTED_EDGE ( 'NONE', *, *, #4315, .F. ) ;
#4355=DIRECTION ( 'NONE',  ( 1.000000000000000000, -0.000000000000000000, -0.000000000000000000 ) ) ;
#4357=EDGE_LOOP ( 'NONE', ( #662, #5524, #1044, #423 ) ) ;
#4360=AXIS2_PLACEMENT_3D ( 'NONE', #6267, #5078, #6310 ) ;
#4366=LINE ( 'NONE', #7278, #220 ) ;
#4369=CARTESIAN_POINT ( 'NONE',  ( 49.98952410273115987, 24.81497846033548527, 10.00000000000000178 ) ) ;
#4370=FACE_OUTER_BOUND ( 'NONE', #7231, .T. ) ;
#4371=AXIS2_PLACEMENT_3D ( 'NONE', #6211, #7516, #2864 ) ;
#4375=DIRECTION ( 'NONE',  ( -0.000000000000000000, -1.000000000000000000, -0.000000000000000000 ) ) ;
#4376=ADVANCED_FACE ( 'NONE', ( #464 ), #6928, .F. ) ;
#4377=EDGE_CURVE ( 'NONE', #3, #6696, #6462, .T. ) ;
#4383=LINE ( 'NONE', #2065, #6266 ) ;
#4386=ORIENTED_EDGE ( 'NONE', *, *, #2526, .F. ) ;
#4390=DIRECTION ( 'NONE',  ( -0.000000000000000000, 1.000000000000000000, 0.000000000000000000 ) ) ;
#4400=EDGE_LOOP ( 'NONE', ( #3302, #5040, #6186, #4254 ) ) ;
#4403=CARTESIAN_POINT ( 'NONE',  ( 47.42432064489011623, 27.28271252672780989, 10.00000000000750155 ) ) ;
#4405=ORIENTED_EDGE ( 'NONE', *, *, #682, .T. ) ;
#4406=FACE_OUTER_BOUND ( 'NONE', #1581, .T. ) ;
#4407=DIRECTION ( 'NONE',  ( -0.000000000000000000, 1.000000000000000000, -0.000000000000000000 ) ) ;
#4408=FACE_OUTER_BOUND ( 'NONE', #501, .T. ) ;
#4410=CARTESIAN_POINT ( 'NONE',  ( 220.0000000000000000, 60.00000000000000000, 3.000000000000021760 ) ) ;
#4411=EDGE_CURVE ( 'NONE', #6942, #5661, #5397, .T. ) ;
#4414=CARTESIAN_POINT ( 'NONE',  ( 220.0000000000000000, -3.000000000000000000, 18.00000000000001066 ) ) ;
#4415=VERTEX_POINT ( 'NONE', #2196 ) ;
#4419=DIRECTION ( 'NONE',  ( 0.000000000000000000, 0.000000000000000000, -1.000000000000000000 ) ) ;
#4422=CARTESIAN_POINT ( 'NONE',  ( 53.00000000000000711, 20.99999999999999645, 10.00000000000001066 ) ) ;
#4425=EDGE_LOOP ( 'NONE', ( #211, #3882, #6932, #6473 ) ) ;
#4427=VECTOR ( 'NONE', #4294, 1000.000000000000114 ) ;
#4430=ORIENTED_EDGE ( 'NONE', *, *, #6132, .F. ) ;
#4433=AXIS2_PLACEMENT_3D ( 'NONE', #2981, #2522, #4875 ) ;
#4435=LINE ( 'NONE', #1386, #2182 ) ;
#4444=EDGE_CURVE ( 'NONE', #4091, #6696, #5777, .T. ) ;
#4446=CYLINDRICAL_SURFACE ( 'NONE', #90, 3.000000000000001332 ) ;
#4447=CARTESIAN_POINT ( 'NONE',  ( 186.7220223217026671, 5.338718410048599594, 14.68135996373468899 ) ) ;
#4449=CYLINDRICAL_SURFACE ( 'NONE', #7003, 13.99999999999999112 ) ;
#4452=EDGE_CURVE ( 'NONE', #4834, #1465, #3139, .T. ) ;
#4453=VERTEX_POINT ( 'NONE', #3470 ) ;
#4454=EDGE_LOOP ( 'NONE', ( #7075, #5564, #6474, #3508 ) ) ;
#4457=CARTESIAN_POINT ( 'NONE',  ( 0.000000000000000000, -56.99999999999999289, 3.000000000000000444 ) ) ;
#4458=DIRECTION ( 'NONE',  ( 0.000000000000000000, 0.000000000000000000, 1.000000000000000000 ) ) ;
#4460=ORIENTED_EDGE ( 'NONE', *, *, #1037, .T. ) ;
#4462=ORIENTED_EDGE ( 'NONE', *, *, #5880, .F. ) ;
#4463=CIRCLE ( 'NONE', #6434, 3.000000000000000000 ) ;
#4465=EDGE_LOOP ( 'NONE', ( #6297, #6117, #6704, #3383 ) ) ;
#4466=LINE ( 'NONE', #276, #6530 ) ;
#4469=CIRCLE ( 'NONE', #7552, 7.000000000000020428 ) ;
#4470=AXIS2_PLACEMENT_3D ( 'NONE', #3995, #3428, #6913 ) ;
#4472=CARTESIAN_POINT ( 'NONE',  ( 220.0000000000000000, 9.000000000000001776, 15.00000000000000888 ) ) ;
#4473=DIRECTION ( 'NONE',  ( 1.000000000000000000, 0.000000000000000000, 0.000000000000000000 ) ) ;
#4483=ORIENTED_EDGE ( 'NONE', *, *, #4245, .T. ) ;
#4491=CARTESIAN_POINT ( 'NONE',  ( 3.000000000000002665, 24.90486745229362953, 37.17889356869155648 ) ) ;
#4492=DIRECTION ( 'NONE',  ( -1.000000000000000000, -0.000000000000000000, -0.000000000000000000 ) ) ;
#4498=DIRECTION ( 'NONE',  ( 0.000000000000000000, 0.000000000000000000, -1.000000000000000000 ) ) ;
#4502=ADVANCED_FACE ( 'NONE', ( #498 ), #7600, .T. ) ;
#4504=LINE ( 'NONE', #6347, #3102 ) ;
#4505=EDGE_LOOP ( 'NONE', ( #5044, #32, #5754, #7529 ) ) ;
#4507=VECTOR ( 'NONE', #7409, 1000.000000000000000 ) ;
#4508=EDGE_CURVE ( 'NONE', #2730, #1997, #7537, .T. ) ;
#4511=CARTESIAN_POINT ( 'NONE',  ( 49.66759159866629858, -24.31912682366575140, 9.999999999997966071 ) ) ;
#4512=DIRECTION ( 'NONE',  ( 0.000000000000000000, 0.000000000000000000, -1.000000000000000000 ) ) ;
#4513=ORIENTED_EDGE ( 'NONE', *, *, #6101, .T. ) ;
#4515=LINE ( 'NONE', #3934, #3370 ) ;
#4520=CARTESIAN_POINT ( 'NONE',  ( 0.000000000000000000, -22.78897920707096247, 12.79060301978498160 ) ) ;
#4521=ADVANCED_FACE ( 'NONE', ( #5240 ), #5890, .T. ) ;
#4523=EDGE_CURVE ( 'NONE', #429, #496, #2643, .T. ) ;
#4525=EDGE_LOOP ( 'NONE', ( #7230, #3360, #5082, #1354 ) ) ;
#4537=ORIENTED_EDGE ( 'NONE', *, *, #2439, .F. ) ;
#4539=FACE_OUTER_BOUND ( 'NONE', #1576, .T. ) ;
#4541=DIRECTION ( 'NONE',  ( 1.000000000000000000, 0.000000000000000000, 0.000000000000000000 ) ) ;
#4545=ORIENTED_EDGE ( 'NONE', *, *, #656, .T. ) ;
#4548=LINE ( 'NONE', #6886, #4319 ) ;
#4551=VECTOR ( 'NONE', #4067, 1000.000000000000000 ) ;
#4552=LINE ( 'NONE', #2928, #6805 ) ;
#4554=ORIENTED_EDGE ( 'NONE', *, *, #2430, .T. ) ;
#4557=DIRECTION ( 'NONE',  ( 0.000000000000000000, 0.000000000000000000, -1.000000000000000000 ) ) ;
#4559=VERTEX_POINT ( 'NONE', #4632 ) ;
#4561=VECTOR ( 'NONE', #1739, 1000.000000000000114 ) ;
#4564=CARTESIAN_POINT ( 'NONE',  ( 49.99999999999998579, 30.03170604878415162, 10.00000000000001243 ) ) ;
#4573=ADVANCED_FACE ( 'NONE', ( #3438 ), #1770, .F. ) ;
#4574=EDGE_LOOP ( 'NONE', ( #4047, #7087, #2357, #5233 ) ) ;
#4576=CARTESIAN_POINT ( 'NONE',  ( 217.0000000000000000, 56.99999999999999289, 7.000000000000022204 ) ) ;
#4578=FACE_OUTER_BOUND ( 'NONE', #1838, .T. ) ;
#4580=VECTOR ( 'NONE', #2231, 1000.000000000000000 ) ;
#4590=VERTEX_POINT ( 'NONE', #6971 ) ;
#4593=ORIENTED_EDGE ( 'NONE', *, *, #4102, .T. ) ;
#4597=CARTESIAN_POINT ( 'NONE',  ( 0.000000000000000000, 0.000000000000000000, 35.00000000000000000 ) ) ;
#4599=ORIENTED_EDGE ( 'NONE', *, *, #7454, .F. ) ;
#4600=CARTESIAN_POINT ( 'NONE',  ( 3.000000000000002665, 30.03170604878415162, 13.00000000000001066 ) ) ;
#4604=ADVANCED_FACE ( 'NONE', ( #6550 ), #4349, .T. ) ;
#4607=LINE ( 'NONE', #3457, #612 ) ;
#4610=VECTOR ( 'NONE', #7497, 1000.000000000000000 ) ;
#4612=TOROIDAL_SURFACE ( 'NONE', #7548, 6.000000000000000000, 3.000000000000000000 ) ;
#4614=VERTEX_POINT ( 'NONE', #1957 ) ;
#4615=CARTESIAN_POINT ( 'NONE',  ( 3.000000000000002665, -60.00000000000000000, 0.000000000000000000 ) ) ;
#4617=CIRCLE ( 'NONE', #1290, 3.000000000000000444 ) ;
#4619=CARTESIAN_POINT ( 'NONE',  ( 217.0000000000000000, -15.08392021690037943, 12.00000000000000711 ) ) ;
#4622=CARTESIAN_POINT ( 'NONE',  ( 186.0399638286351376, -8.214460233858028815, 13.50000000000791012 ) ) ;
#4623=EDGE_CURVE ( 'NONE', #6273, #5270, #2626, .T. ) ;
#4625=ORIENTED_EDGE ( 'NONE', *, *, #2353, .T. ) ;
#4631=CARTESIAN_POINT ( 'NONE',  ( 217.0000000000000000, 56.99999999999999289, 7.000000000000022204 ) ) ;
#4632=CARTESIAN_POINT ( 'NONE',  ( 217.0000000000000000, 18.04196010845019060, 12.50000000000000711 ) ) ;
#4636=CARTESIAN_POINT ( 'NONE',  ( 217.0000000000000000, 56.99999999999999289, 10.00000000000002132 ) ) ;
#4638=ORIENTED_EDGE ( 'NONE', *, *, #3630, .T. ) ;
#4640=CARTESIAN_POINT ( 'NONE',  ( 217.0000000000000000, -2.312964634635744633E-15, 7.000000000000002665 ) ) ;
#4644=ORIENTED_EDGE ( 'NONE', *, *, #7222, .T. ) ;
#4645=EDGE_CURVE ( 'NONE', #2786, #2919, #5681, .T. ) ;
#4651=LINE ( 'NONE', #1710, #4551 ) ;
#4653=EDGE_CURVE ( 'NONE', #3524, #2601, #5725, .T. ) ;
#4659=DIRECTION ( 'NONE',  ( -0.4999999999999976130, -0.000000000000000000, -0.8660254037844399289 ) ) ;
#4667=CARTESIAN_POINT ( 'NONE',  ( 50.01367358680484188, -23.17418217178283868, 9.999999999989126920 ) ) ;
#4669=ORIENTED_EDGE ( 'NONE', *, *, #1814, .F. ) ;
#4675=EDGE_CURVE ( 'NONE', #1932, #6366, #2783, .T. ) ;
#4677=DIRECTION ( 'NONE',  ( -0.000000000000000000, -0.000000000000000000, 1.000000000000000000 ) ) ;
#4678=CYLINDRICAL_SURFACE ( 'NONE', #901, 2.999999999999999112 ) ;
#4684=CARTESIAN_POINT ( 'NONE',  ( 50.51471862576143224, 30.03170604878414807, 10.00000000000001066 ) ) ;
#4690=VECTOR ( 'NONE', #285, 1000.000000000000114 ) ;
#4694=CARTESIAN_POINT ( 'NONE',  ( 3.000000000000000000, -56.99999999999999289, 3.000000000000000444 ) ) ;
#4696=DIRECTION ( 'NONE',  ( -1.000000000000000000, -0.000000000000000000, -0.000000000000000000 ) ) ;
#4697=DIRECTION ( 'NONE',  ( 0.000000000000000000, 0.000000000000000000, 1.000000000000000000 ) ) ;
#4698=ADVANCED_FACE ( 'NONE', ( #3318 ), #5664, .T. ) ;
#4701=DIRECTION ( 'NONE',  ( 0.000000000000000000, -0.000000000000000000, 1.000000000000000000 ) ) ;
#4704=ORIENTED_EDGE ( 'NONE', *, *, #4645, .F. ) ;
#4707=CARTESIAN_POINT ( 'NONE',  ( 47.40604585759381706, -25.88825784476160052, 9.999999999998642863 ) ) ;
#4711=VECTOR ( 'NONE', #1500, 1000.000000000000114 ) ;
#4716=CARTESIAN_POINT ( 'NONE',  ( 220.0000000000000000, -9.000000000000001776, 12.00000000000000888 ) ) ;
#4718=ADVANCED_FACE ( 'NONE', ( #2485 ), #5683, .F. ) ;
#4719=ORIENTED_EDGE ( 'NONE', *, *, #2213, .F. ) ;
#4724=CARTESIAN_POINT ( 'NONE',  ( 217.0000000000000000, 56.99999999999999289, 7.000000000000021316 ) ) ;
#4726=LINE ( 'NONE', #4147, #7364 ) ;
#4729=VERTEX_POINT ( 'NONE', #5202 ) ;
#4730=DIRECTION ( 'NONE',  ( 0.000000000000000000, 0.000000000000000000, 1.000000000000000000 ) ) ;
#4732=DIRECTION ( 'NONE',  ( -0.4999999999999967804, 2.003086131649549845E-15, -0.8660254037844405950 ) ) ;
#4733=DIRECTION ( 'NONE',  ( -0.000000000000000000, 1.000000000000000000, -0.000000000000000000 ) ) ;
#4734=CARTESIAN_POINT ( 'NONE',  ( 189.3320144560679239, -7.156359838973473941, 15.60099947390724928 ) ) ;
#4737=AXIS2_PLACEMENT_3D ( 'NONE', #1819, #1700, #5933 ) ;
#4738=VERTEX_POINT ( 'NONE', #4636 ) ;
#4741=ADVANCED_BREP_SHAPE_REPRESENTATION ( '', ( #6351, #1914 ), #1662 ) ;
#4744=VECTOR ( 'NONE', #1801, 1000.000000000000114 ) ;
#4749=DIRECTION ( 'NONE',  ( 0.000000000000000000, -1.000000000000000000, 0.000000000000000000 ) ) ;
#4750=DIRECTION ( 'NONE',  ( -1.000000000000000000, -0.000000000000000000, -0.000000000000000000 ) ) ;
#4752=ORIENTED_EDGE ( 'NONE', *, *, #2807, .F. ) ;
#4755=CARTESIAN_POINT ( 'NONE',  ( 47.00000000000000000, -25.78715168812825098, 12.89530150989249435 ) ) ;
#4758=DIRECTION ( 'NONE',  ( -0.000000000000000000, -0.000000000000000000, 1.000000000000000000 ) ) ;
#4762=CARTESIAN_POINT ( 'NONE',  ( 3.000000000000002665, 60.00000000000000000, 2.204364238465235507E-14 ) ) ;
#4764=CARTESIAN_POINT ( 'NONE',  ( 220.0000000000000000, -3.000000000000000888, 35.00000000000000000 ) ) ;
#4765=AXIS2_PLACEMENT_3D ( 'NONE', #6077, #7229, #6651 ) ;
#4768=CARTESIAN_POINT ( 'NONE',  ( 188.6380400399839061, 7.242640687119284770, 15.00000000000001066 ) ) ;
#4770=ORIENTED_EDGE ( 'NONE', *, *, #6184, .F. ) ;
#4776=DIRECTION ( 'NONE',  ( 1.000000000000000000, 0.000000000000000000, 0.000000000000000000 ) ) ;
#4779=ORIENTED_EDGE ( 'NONE', *, *, #207, .F. ) ;
#4780=CARTESIAN_POINT ( 'NONE',  ( 193.5000000000000000, -39.99999999999999289, 0.000000000000000000 ) ) ;
#4781=CARTESIAN_POINT ( 'NONE',  ( 3.000000000000002665, -56.99999999999999289, 3.000000000000000444 ) ) ;
#4787=EDGE_LOOP ( 'NONE', ( #3239, #938 ) ) ;
#4791=ORIENTED_EDGE ( 'NONE', *, *, #4932, .T. ) ;
#4793=CARTESIAN_POINT ( 'NONE',  ( 185.0000000000000000, -39.99999999999999289, 0.000000000000000000 ) ) ;
#4794=CARTESIAN_POINT ( 'NONE',  ( 220.0000000000000000, -15.00000000000000355, 12.00000000000000711 ) ) ;
#4796=DIRECTION ( 'NONE',  ( 1.000000000000000000, 0.000000000000000000, 0.000000000000000000 ) ) ;
#4799=FACE_OUTER_BOUND ( 'NONE', #4400, .T. ) ;
#4800=DIRECTION ( 'NONE',  ( 0.000000000000000000, 0.000000000000000000, -1.000000000000000000 ) ) ;
#4801=ADVANCED_FACE ( 'NONE', ( #2201 ), #2778, .T. ) ;
#4806=CARTESIAN_POINT ( 'NONE',  ( 187.5208830142895238, 7.524469495810456543, 15.00000000000001243 ) ) ;
#4810=EDGE_CURVE ( 'NONE', #7468, #597, #4552, .T. ) ;
#4811=EDGE_LOOP ( 'NONE', ( #1890, #3327, #3328 ) ) ;
#4813=VECTOR ( 'NONE', #209, 1000.000000000000000 ) ;
#4827=CARTESIAN_POINT ( 'NONE',  ( 217.0000000000000000, 15.08392021690038121, 15.00000000000000888 ) ) ;
#4831=DIRECTION ( 'NONE',  ( 0.000000000000000000, 0.03489949670250346025, 0.9993908270190956511 ) ) ;
#4834=VERTEX_POINT ( 'NONE', #5703 ) ;
#4836=CARTESIAN_POINT ( 'NONE',  ( 3.000000000000002665, 56.99999999999999289, 2.204364238465235507E-14 ) ) ;
#4838=AXIS2_PLACEMENT_3D ( 'NONE', #2857, #6557, #5866 ) ;
#4845=CARTESIAN_POINT ( 'NONE',  ( 186.7339382447161711, -5.312719677946581065, 14.70199894781319649 ) ) ;
#4846=CIRCLE ( 'NONE', #3241, 3.000000000000000000 ) ;
#4852=EDGE_CURVE ( 'NONE', #6942, #2264, #4515, .T. ) ;
#4858=AXIS2_PLACEMENT_3D ( 'NONE', #265, #2684, #7302 ) ;
#4868=CARTESIAN_POINT ( 'NONE',  ( 50.00000000000000000, 0.000000000000000000, 35.00000000000000000 ) ) ;
#4872=CARTESIAN_POINT ( 'NONE',  ( 209.9999999999999716, 6.000000000000000000, 35.00000000000000000 ) ) ;
#4874=DIRECTION ( 'NONE',  ( 0.000000000000000000, 0.000000000000000000, 1.000000000000000000 ) ) ;
#4875=DIRECTION ( 'NONE',  ( 0.000000000000000000, 0.000000000000000000, -1.000000000000000000 ) ) ;
#4879=CIRCLE ( 'NONE', #6836, 2.999999999999999112 ) ;
#4881=FACE_OUTER_BOUND ( 'NONE', #6900, .T. ) ;
#4882=DIRECTION ( 'NONE',  ( 0.000000000000000000, 0.000000000000000000, -1.000000000000000000 ) ) ;
#4885=EDGE_CURVE ( 'NONE', #7378, #5359, #4131, .T. ) ;
#4886=EDGE_LOOP ( 'NONE', ( #2210, #3076, #3718, #3845, #7081, #5735, #4342 ) ) ;
#4891=CARTESIAN_POINT ( 'NONE',  ( 35.00000000000000000, -39.99999999999999289, 0.000000000000000000 ) ) ;
#4901=FACE_BOUND ( 'NONE', #1427, .T. ) ;
#4904=ADVANCED_FACE ( 'NONE', ( #6621 ), #7421, .T. ) ;
#4907=ORIENTED_EDGE ( 'NONE', *, *, #4444, .F. ) ;
#4909=DIRECTION ( 'NONE',  ( -0.000000000000000000, 0.000000000000000000, 1.000000000000000000 ) ) ;
#4911=ORIENTED_EDGE ( 'NONE', *, *, #7361, .T. ) ;
#4915=CARTESIAN_POINT ( 'NONE',  ( 217.0000000000000000, -56.99999999999999289, 5.510910596163094486E-16 ) ) ;
#4930=ORIENTED_EDGE ( 'NONE', *, *, #4885, .T. ) ;
#4931=EDGE_LOOP ( 'NONE', ( #4644, #7354, #3440, #5771 ) ) ;
#4932=EDGE_CURVE ( 'NONE', #3769, #734, #3633, .T. ) ;
#4933=CYLINDRICAL_SURFACE ( 'NONE', #52, 25.00000000000000000 ) ;
#4937=AXIS2_PLACEMENT_3D ( 'NONE', #2848, #5239, #497 ) ;
#4941=ORIENTED_EDGE ( 'NONE', *, *, #2032, .T. ) ;
#4942=AXIS2_PLACEMENT_3D ( 'NONE', #4694, #7029, #1363 ) ;
#4944=CARTESIAN_POINT ( 'NONE',  ( 52.84383605862925748, 25.58527333940346082, 10.00000000000000888 ) ) ;
#4945=CARTESIAN_POINT ( 'NONE',  ( 217.0000000000000000, -60.00000000000000000, 0.000000000000000000 ) ) ;
#4948=DIRECTION ( 'NONE',  ( 0.000000000000000000, 0.000000000000000000, -1.000000000000000000 ) ) ;
#4949=EDGE_CURVE ( 'NONE', #7465, #510, #1343, .T. ) ;
#4952=LINE ( 'NONE', #7286, #5162 ) ;
#4953=ORIENTED_EDGE ( 'NONE', *, *, #6739, .T. ) ;
#4957=VERTEX_POINT ( 'NONE', #6476 ) ;
#4958=DIRECTION ( 'NONE',  ( -0.000000000000000000, 1.000000000000000000, 2.065146995210484941E-16 ) ) ;
#4961=CARTESIAN_POINT ( 'NONE',  ( 220.0000000000000000, -60.00000000000000000, 3.000000000000000888 ) ) ;
#4962=DIRECTION ( 'NONE',  ( 0.000000000000000000, 0.000000000000000000, -1.000000000000000000 ) ) ;
#4964=AXIS2_PLACEMENT_3D ( 'NONE', #6204, #2093, #3326 ) ;
#4967=ORIENTED_EDGE ( 'NONE', *, *, #1617, .T. ) ;
#4980=ORIENTED_EDGE ( 'NONE', *, *, #5920, .T. ) ;
#4983=AXIS2_PLACEMENT_3D ( 'NONE', #6916, #3888, #2718 ) ;
#4984=AXIS2_PLACEMENT_3D ( 'NONE', #5816, #4167, #2888 ) ;
#4987=CIRCLE ( 'NONE', #1907, 10.00000000000001954 ) ;
#4992=CARTESIAN_POINT ( 'NONE',  ( 220.0000000000000000, -9.000000000000001776, 18.00000000000001066 ) ) ;
#4993=ORIENTED_EDGE ( 'NONE', *, *, #4653, .T. ) ;
#4994=ORIENTED_EDGE ( 'NONE', *, *, #2468, .F. ) ;
#4995=EDGE_CURVE ( 'NONE', #1465, #4834, #2741, .T. ) ;
#4996=DIRECTION ( 'NONE',  ( -1.000000000000000000, 0.000000000000000000, 0.000000000000000000 ) ) ;
#5000=CARTESIAN_POINT ( 'NONE',  ( 188.6380400399839061, -9.000000000000001776, 15.00000000000000888 ) ) ;
#5004=EDGE_CURVE ( 'NONE', #3862, #3547, #3325, .T. ) ;
#5008=FACE_OUTER_BOUND ( 'NONE', #830, .T. ) ;
#5009=AXIS2_PLACEMENT_3D ( 'NONE', #5025, #7288, #6749 ) ;
#5016=DIRECTION ( 'NONE',  ( 0.000000000000000000, -0.03489949670250429292, -0.9993908270190955401 ) ) ;
#5020=VERTEX_POINT ( 'NONE', #1234 ) ;
#5024=ORIENTED_EDGE ( 'NONE', *, *, #4377, .T. ) ;
#5025=CARTESIAN_POINT ( 'NONE',  ( 35.00000000000000000, 39.99999999999999289, 0.000000000000000000 ) ) ;
#5027=CARTESIAN_POINT ( 'NONE',  ( 50.00000000000000000, 0.000000000000000000, 48.99999999999999289 ) ) ;
#5029=FACE_OUTER_BOUND ( 'NONE', #7039, .T. ) ;
#5033=VERTEX_POINT ( 'NONE', #129 ) ;
#5040=ORIENTED_EDGE ( 'NONE', *, *, #7155, .T. ) ;
#5043=CARTESIAN_POINT ( 'NONE',  ( 0.000000000000000000, -23.20733648494241663, 0.8104180479081783961 ) ) ;
#5044=ORIENTED_EDGE ( 'NONE', *, *, #4508, .F. ) ;
#5054=CARTESIAN_POINT ( 'NONE',  ( 220.0000000000000000, 56.99999999999999289, 3.000000000000021316 ) ) ;
#5055=VERTEX_POINT ( 'NONE', #7312 ) ;
#5058=EDGE_CURVE ( 'NONE', #2795, #3993, #6734, .T. ) ;
#5059=CARTESIAN_POINT ( 'NONE',  ( 193.5000000000000000, 39.99999999999999289, 0.000000000000000000 ) ) ;
#5061=CARTESIAN_POINT ( 'NONE',  ( 47.00000000000000000, -21.98659819442010388, 35.76778892745510063 ) ) ;
#5063=FACE_OUTER_BOUND ( 'NONE', #7471, .T. ) ;
#5064=CARTESIAN_POINT ( 'NONE',  ( 188.6380400399839061, 9.000000000000001776, 15.00000000000000888 ) ) ;
#5068=ADVANCED_FACE ( 'NONE', ( #5583 ), #4933, .T. ) ;
#5072=CARTESIAN_POINT ( 'NONE',  ( 3.000000000000002665, -60.00000000000000000, 7.000000000000000888 ) ) ;
#5078=DIRECTION ( 'NONE',  ( 0.000000000000000000, -1.000000000000000000, -0.000000000000000000 ) ) ;
#5080=CARTESIAN_POINT ( 'NONE',  ( 220.0000000000000000, -15.08392021690038298, 15.00000000000000888 ) ) ;
#5082=ORIENTED_EDGE ( 'NONE', *, *, #1521, .F. ) ;
#5084=CIRCLE ( 'NONE', #43, 2.999999999999999556 ) ;
#5085=EDGE_CURVE ( 'NONE', #5661, #4957, #1830, .T. ) ;
#5087=CARTESIAN_POINT ( 'NONE',  ( 49.52414331456670027, 25.96382905951872644, 9.999999999999324984 ) ) ;
#5094=FACE_OUTER_BOUND ( 'NONE', #2687, .T. ) ;
#5096=CARTESIAN_POINT ( 'NONE',  ( 0.000000000000000000, -21.98659819442010388, 35.76778892745510063 ) ) ;
#5098=ORIENTED_EDGE ( 'NONE', *, *, #6607, .F. ) ;
#5102=CIRCLE ( 'NONE', #428, 3.000000000000000000 ) ;
#5107=CARTESIAN_POINT ( 'NONE',  ( 3.000000000000002665, 56.99999999999999289, 10.00000000000002132 ) ) ;
#5110=CIRCLE ( 'NONE', #2889, 8.500000000000007105 ) ;
#5116=LINE ( 'NONE', #299, #4507 ) ;
#5120=EDGE_LOOP ( 'NONE', ( #5451, #2721, #342, #7298 ) ) ;
#5122=CYLINDRICAL_SURFACE ( 'NONE', #3255, 10.00000000000001954 ) ;
#5124=CARTESIAN_POINT ( 'NONE',  ( 50.68728032241775594, -27.58259254939923721, 10.00000000000000533 ) ) ;
#5125=CARTESIAN_POINT ( 'NONE',  ( 50.29734716306172970, -18.29734716306171549, 10.98910980934740778 ) ) ;
#5129=DIRECTION ( 'NONE',  ( 1.000000000000000000, 0.000000000000000000, 0.000000000000000000 ) ) ;
#5130=ORIENTED_EDGE ( 'NONE', *, *, #7595, .F. ) ;
#5134=CYLINDRICAL_SURFACE ( 'NONE', #1385, 3.000000000000007994 ) ;
#5137=ORIENTED_EDGE ( 'NONE', *, *, #5605, .F. ) ;
#5139=PLANE ( 'NONE',  #4272 ) ;
#5147=ORIENTED_EDGE ( 'NONE', *, *, #3942, .F. ) ;
#5148=ORIENTED_EDGE ( 'NONE', *, *, #3314, .F. ) ;
#5152=DIRECTION ( 'NONE',  ( 1.000000000000000000, 0.000000000000000000, 0.000000000000000000 ) ) ;
#5155=ORIENTED_EDGE ( 'NONE', *, *, #1775, .F. ) ;
#5158=CARTESIAN_POINT ( 'NONE',  ( 3.000000000000002665, 24.90486745229362953, 37.17889356869155648 ) ) ;
#5162=VECTOR ( 'NONE', #4375, 1000.000000000000000 ) ;
#5163=EDGE_CURVE ( 'NONE', #1140, #2192, #2612, .T. ) ;
#5168=CARTESIAN_POINT ( 'NONE',  ( 3.000000000000002665, -22.78897920707096247, 12.79060301978498160 ) ) ;
#5169=AXIS2_PLACEMENT_3D ( 'NONE', #6592, #3558, #2398 ) ;
#5172=ORIENTED_EDGE ( 'NONE', *, *, #7157, .T. ) ;
#5175=DIRECTION ( 'NONE',  ( 0.000000000000000000, 0.000000000000000000, 1.000000000000000000 ) ) ;
#5178=CARTESIAN_POINT ( 'NONE',  ( 187.9839735574547603, 6.029117148349426358, 16.86712362072634264 ) ) ;
#5189=DIRECTION ( 'NONE',  ( 0.000000000000000000, -0.000000000000000000, -1.000000000000000000 ) ) ;
#5190=CYLINDRICAL_SURFACE ( 'NONE', #2395, 8.500000000000007105 ) ;
#5191=CARTESIAN_POINT ( 'NONE',  ( 186.0399638286305901, -9.000000000000001776, 13.50000000000000178 ) ) ;
#5195=CARTESIAN_POINT ( 'NONE',  ( 217.0000000000000000, -56.99999999999999289, 7.000000000000000000 ) ) ;
#5199=EDGE_CURVE ( 'NONE', #797, #1980, #3468, .T. ) ;
#5202=CARTESIAN_POINT ( 'NONE',  ( 209.9999999999999716, 6.000000000000000000, 41.00000000000002132 ) ) ;
#5206=CARTESIAN_POINT ( 'NONE',  ( 3.000000000000000000, 56.99999999999999289, 3.000000000000021760 ) ) ;
#5211=ORIENTED_EDGE ( 'NONE', *, *, #2405, .T. ) ;
#5216=LINE ( 'NONE', #673, #1162 ) ;
#5226=FACE_OUTER_BOUND ( 'NONE', #1547, .T. ) ;
#5232=EDGE_CURVE ( 'NONE', #1421, #459, #3504, .T. ) ;
#5233=ORIENTED_EDGE ( 'NONE', *, *, #3899, .F. ) ;
#5237=DIRECTION ( 'NONE',  ( 1.000000000000000000, 0.000000000000000000, 0.000000000000000000 ) ) ;
#5238=ORIENTED_EDGE ( 'NONE', *, *, #4852, .T. ) ;
#5239=DIRECTION ( 'NONE',  ( -1.000000000000000000, -0.000000000000000000, -0.000000000000000000 ) ) ;
#5240=FACE_OUTER_BOUND ( 'NONE', #2566, .T. ) ;
#5246=EDGE_LOOP ( 'NONE', ( #6045, #2472, #4128, #7016 ) ) ;
#5248=CARTESIAN_POINT ( 'NONE',  ( 43.50000000000001421, 39.99999999999999289, 0.000000000000000000 ) ) ;
#5249=CARTESIAN_POINT ( 'NONE',  ( 47.00000000000000000, 30.03170604878415162, 13.00000000000001066 ) ) ;
#5251=EDGE_LOOP ( 'NONE', ( #5854, #6510, #3235, #2321 ) ) ;
#5253=DIRECTION ( 'NONE',  ( -1.000000000000000000, -0.000000000000000000, -0.000000000000000000 ) ) ;
#5258=B_SPLINE_CURVE_WITH_KNOTS ( 'NONE', 3,
 ( #5000, #294, #6137, #7367, #3802, #979, #1446, #2640, #1477, #2100 ),
 .UNSPECIFIED., .F., .F.,
 ( 4, 2, 2, 2, 4 ),
 ( -1.095445419986480569E-05, 0.001102508244345350684, 0.002215970942890566238, 0.003329433641435781792, 0.004442896339980997346 ),
 .UNSPECIFIED. ) ;
#5265=CARTESIAN_POINT ( 'NONE',  ( 217.0000000000000000, 15.00000000000000000, 15.00000000000000888 ) ) ;
#5266=LINE ( 'NONE', #2451, #2525 ) ;
#5268=EDGE_CURVE ( 'NONE', #1421, #1604, #3966, .T. ) ;
#5269=CARTESIAN_POINT ( 'NONE',  ( 188.2950735375078750, -5.838146261106893498, 17.40596459241342231 ) ) ;
#5270=VERTEX_POINT ( 'NONE', #1651 ) ;
#5281=CARTESIAN_POINT ( 'NONE',  ( 53.00000000000000711, -20.99999999999999645, 10.00000000000000888 ) ) ;
#5282=ORIENTED_EDGE ( 'NONE', *, *, #5531, .T. ) ;
#5286=DIRECTION ( 'NONE',  ( -0.8660254037844413721, 0.000000000000000000, 0.4999999999999950595 ) ) ;
#5292=DIRECTION ( 'NONE',  ( -0.000000000000000000, 1.000000000000000000, 2.065146995210484941E-16 ) ) ;
#5294=EDGE_CURVE ( 'NONE', #2976, #2821, #7427, .T. ) ;
#5296=ORIENTED_EDGE ( 'NONE', *, *, #6500, .F. ) ;
#5297=CARTESIAN_POINT ( 'NONE',  ( 209.9999999999999716, -6.000000000000000000, 18.00000000000001066 ) ) ;
#5298=CARTESIAN_POINT ( 'NONE',  ( 220.0000000000000000, 9.000000000000001776, 18.00000000000001066 ) ) ;
#5299=CARTESIAN_POINT ( 'NONE',  ( 187.2209186502361149, 6.851382254476026112, 15.00000000000001066 ) ) ;
#5300=CIRCLE ( 'NONE', #4937, 25.00000000000000000 ) ;
#5302=EDGE_CURVE ( 'NONE', #3744, #6935, #3129, .T. ) ;
#5310=CARTESIAN_POINT ( 'NONE',  ( 48.51085693943327470, -25.40781859939735199, 12.90851588443849174 ) ) ;
#5312=VERTEX_POINT ( 'NONE', #532 ) ;
#5313=AXIS2_PLACEMENT_3D ( 'NONE', #7227, #4310, #7342 ) ;
#5321=DIRECTION ( 'NONE',  ( 0.000000000000000000, -3.304235192336777977E-16, 1.000000000000000000 ) ) ;
#5322=VERTEX_POINT ( 'NONE', #997 ) ;
#5323=EDGE_CURVE ( 'NONE', #6005, #1310, #422, .T. ) ;
#5325=DIRECTION ( 'NONE',  ( 1.000000000000000000, 0.000000000000000000, 0.000000000000000000 ) ) ;
#5326=ORIENTED_EDGE ( 'NONE', *, *, #6654, .T. ) ;
#5329=DIRECTION ( 'NONE',  ( 0.000000000000000000, 0.000000000000000000, -1.000000000000000000 ) ) ;
#5330=DIRECTION ( 'NONE',  ( -1.000000000000000000, -0.000000000000000000, -0.000000000000000000 ) ) ;
#5337=CARTESIAN_POINT ( 'NONE',  ( 0.000000000000000000, 27.04312195450891565, 12.73853277175702559 ) ) ;
#5339=CARTESIAN_POINT ( 'NONE',  ( 3.000000000000002665, -22.89008536370703695, 9.895301509892497904 ) ) ;
#5341=ADVANCED_FACE ( 'NONE', ( #5774 ), #5122, .T. ) ;
#5342=CARTESIAN_POINT ( 'NONE',  ( 217.0000000000000000, 15.08392021690038121, 12.00000000000000711 ) ) ;
#5344=AXIS2_PLACEMENT_3D ( 'NONE', #5195, #3435, #5656 ) ;
#5346=VECTOR ( 'NONE', #5189, 1000.000000000000000 ) ;
#5349=VECTOR ( 'NONE', #2875, 1000.000000000000000 ) ;
#5351=CIRCLE ( 'NONE', #796, 2.999999999999999112 ) ;
#5358=CARTESIAN_POINT ( 'NONE',  ( 26.49999999999999645, -39.99999999999999289, 0.000000000000000000 ) ) ;
#5359=VERTEX_POINT ( 'NONE', #2846 ) ;
#5366=CARTESIAN_POINT ( 'NONE',  ( 220.0000000000000000, 3.000000000000000000, 35.00000000000000000 ) ) ;
#5369=AXIS2_PLACEMENT_3D ( 'NONE', #194, #834, #1953 ) ;
#5371=CARTESIAN_POINT ( 'NONE',  ( 3.000000000000002665, -60.00000000000000000, 3.000000000000000444 ) ) ;
#5373=DIRECTION ( 'NONE',  ( 0.000000000000000000, -2.065146995210484448E-16, 1.000000000000000000 ) ) ;
#5374=EDGE_CURVE ( 'NONE', #5934, #570, #7544, .T. ) ;
#5376=DIRECTION ( 'NONE',  ( -0.000000000000000000, 1.000000000000000000, -0.000000000000000000 ) ) ;
#5377=ADVANCED_FACE ( 'NONE', ( #649 ), #5923, .T. ) ;
#5378=CARTESIAN_POINT ( 'NONE',  ( 217.0000000000000000, 0.000000000000000000, 12.00000000000000711 ) ) ;
#5392=PLANE ( 'NONE',  #3824 ) ;
#5395=EDGE_CURVE ( 'NONE', #6501, #5696, #6189, .T. ) ;
#5397=( BOUNDED_CURVE ( )  B_SPLINE_CURVE ( 3, ( #5698, #425, #5125, #7467 ),
 .UNSPECIFIED., .F., .T. ) 
 B_SPLINE_CURVE_WITH_KNOTS ( ( 4, 4 ),
 ( 4.712388980384690562, 6.115737227959895606 ),
 .UNSPECIFIED. ) 
 CURVE ( )  GEOMETRIC_REPRESENTATION_ITEM ( )  RATIONAL_B_SPLINE_CURVE ( ( 1.000000000000000000, 0.8425084105506492893, 0.8425084105506492893, 1.000000000000000000 ) ) 
 REPRESENTATION_ITEM ( '' )  );
#5402=CYLINDRICAL_SURFACE ( 'NONE', #6087, 6.000000000000015987 ) ;
#5403=ORIENTED_EDGE ( 'NONE', *, *, #5199, .F. ) ;
#5405=PLANE ( 'NONE',  #5989 ) ;
#5412=VECTOR ( 'NONE', #6527, 1000.000000000000000 ) ;
#5418=DIRECTION ( 'NONE',  ( 0.000000000000000000, 0.000000000000000000, 1.000000000000000000 ) ) ;
#5419=CARTESIAN_POINT ( 'NONE',  ( 191.2361162513372221, -6.000000000000000000, 16.49999999999999289 ) ) ;
#5420=DIRECTION ( 'NONE',  ( -1.000000000000000000, -0.000000000000000000, -0.000000000000000000 ) ) ;
#5421=CARTESIAN_POINT ( 'NONE',  ( 189.5040654437683258, -3.000000000000000888, 19.50000000000000355 ) ) ;
#5422=AXIS2_PLACEMENT_3D ( 'NONE', #6163, #6784, #6710 ) ;
#5425=ORIENTED_EDGE ( 'NONE', *, *, #5294, .T. ) ;
#5431=B_SPLINE_CURVE_WITH_KNOTS ( 'NONE', 3,
 ( #2788, #6445, #1054, #2823 ),
 .UNSPECIFIED., .F., .F.,
 ( 4, 4 ),
 ( 0.000000000000000000, 0.0005182278649586876925 ),
 .UNSPECIFIED. ) ;
#5432=ORIENTED_EDGE ( 'NONE', *, *, #2775, .T. ) ;
#5433=ORIENTED_EDGE ( 'NONE', *, *, #7238, .T. ) ;
#5435=CARTESIAN_POINT ( 'NONE',  ( 3.000000000000002665, -18.00000000000000000, 10.00000000000000888 ) ) ;
#5439=PLANE ( 'NONE',  #3463 ) ;
#5442=ORIENTED_EDGE ( 'NONE', *, *, #242, .F. ) ;
#5445=VERTEX_POINT ( 'NONE', #5885 ) ;
#5448=DIRECTION ( 'NONE',  ( -1.000000000000000000, 0.000000000000000000, 0.000000000000000000 ) ) ;
#5451=ORIENTED_EDGE ( 'NONE', *, *, #1566, .T. ) ;
#5453=CARTESIAN_POINT ( 'NONE',  ( 185.0000000000000000, 39.99999999999999289, 10.00000000000000355 ) ) ;
#5459=AXIS2_PLACEMENT_3D ( 'NONE', #3419, #2257, #5758 ) ;
#5462=CARTESIAN_POINT ( 'NONE',  ( 217.0000000000000000, -20.99999999999999645, 13.00000000000000888 ) ) ;
#5463=AXIS2_PLACEMENT_3D ( 'NONE', #5747, #5820, #467 ) ;
#5465=VECTOR ( 'NONE', #5566, 1000.000000000000000 ) ;
#5474=ORIENTED_EDGE ( 'NONE', *, *, #4043, .F. ) ;
#5479=CARTESIAN_POINT ( 'NONE',  ( 209.9999999999999716, 6.000000000000000000, 35.00000000000000000 ) ) ;
#5481=ORIENTED_EDGE ( 'NONE', *, *, #7525, .T. ) ;
#5483=ADVANCED_FACE ( 'NONE', ( #7038 ), #1765, .F. ) ;
#5486=DIRECTION ( 'NONE',  ( 0.000000000000000000, 0.000000000000000000, 1.000000000000000000 ) ) ;
#5489=EDGE_LOOP ( 'NONE', ( #4638, #6980, #5137, #3623 ) ) ;
#5496=AXIS2_PLACEMENT_3D ( 'NONE', #252, #5175, #7590 ) ;
#5499=ORIENTED_EDGE ( 'NONE', *, *, #756, .F. ) ;
#5507=ORIENTED_EDGE ( 'NONE', *, *, #5605, .T. ) ;
#5508=ORIENTED_EDGE ( 'NONE', *, *, #5004, .T. ) ;
#5510=ADVANCED_FACE ( 'NONE', ( #230 ), #3749, .T. ) ;
#5513=VERTEX_POINT ( 'NONE', #3186 ) ;
#5515=LINE ( 'NONE', #239, #2838 ) ;
#5519=CARTESIAN_POINT ( 'NONE',  ( 203.9378221735088630, 6.000000000000000000, 38.50000000000000000 ) ) ;
#5520=ORIENTED_EDGE ( 'NONE', *, *, #6146, .F. ) ;
#5521=CARTESIAN_POINT ( 'NONE',  ( 217.0000000000000000, -56.99999999999999289, 3.000000000000000444 ) ) ;
#5522=CYLINDRICAL_SURFACE ( 'NONE', #5422, 8.500000000000007105 ) ;
#5523=CARTESIAN_POINT ( 'NONE',  ( 3.000000000000002665, -25.88825784476432545, 10.00000000000001066 ) ) ;
#5524=ORIENTED_EDGE ( 'NONE', *, *, #4001, .F. ) ;
#5529=ORIENTED_EDGE ( 'NONE', *, *, #5302, .T. ) ;
#5531=EDGE_CURVE ( 'NONE', #2238, #2601, #6812, .T. ) ;
#5535=CARTESIAN_POINT ( 'NONE',  ( 47.00000000000000000, -28.78532416918554304, 10.00000000000000711 ) ) ;
#5536=CARTESIAN_POINT ( 'NONE',  ( 217.0000000000000000, -18.00000000000000000, 10.00000000000000888 ) ) ;
#5537=AXIS2_PLACEMENT_3D ( 'NONE', #4640, #3978, #7586 ) ;
#5540=FACE_OUTER_BOUND ( 'NONE', #813, .T. ) ;
#5542=AXIS2_PLACEMENT_3D ( 'NONE', #5787, #587, #2856 ) ;
#5546=ORIENTED_EDGE ( 'NONE', *, *, #5395, .F. ) ;
#5547=AXIS2_PLACEMENT_3D ( 'NONE', #7235, #1199, #625 ) ;
#5552=AXIS2_PLACEMENT_3D ( 'NONE', #5453, #5418, #6570 ) ;
#5555=CARTESIAN_POINT ( 'NONE',  ( 220.0000000000000000, -15.08392021690038121, 12.00000000000000711 ) ) ;
#5559=CARTESIAN_POINT ( 'NONE',  ( 47.00000000000000000, 21.91628335801839356, 36.91742634044857141 ) ) ;
#5560=CARTESIAN_POINT ( 'NONE',  ( 3.000000000000002665, 60.00000000000000000, 3.000000000000021760 ) ) ;
#5562=EDGE_CURVE ( 'NONE', #5749, #3892, #7265, .T. ) ;
#5563=VERTEX_POINT ( 'NONE', #1451 ) ;
#5564=ORIENTED_EDGE ( 'NONE', *, *, #1642, .F. ) ;
#5566=DIRECTION ( 'NONE',  ( -0.000000000000000000, -0.000000000000000000, 1.000000000000000000 ) ) ;
#5567=CARTESIAN_POINT ( 'NONE',  ( 216.9999999999999716, 6.000000000000000000, 35.00000000000000000 ) ) ;
#5569=DIRECTION ( 'NONE',  ( 0.000000000000000000, 0.000000000000000000, 1.000000000000000000 ) ) ;
#5573=ADVANCED_FACE ( 'NONE', ( #1992 ), #5615, .T. ) ;
#5574=DIRECTION ( 'NONE',  ( 0.000000000000000000, 0.000000000000000000, 1.000000000000000000 ) ) ;
#5578=ORIENTED_EDGE ( 'NONE', *, *, #983, .F. ) ;
#5579=VERTEX_POINT ( 'NONE', #6112 ) ;
#5583=FACE_OUTER_BOUND ( 'NONE', #1405, .T. ) ;
#5585=LINE ( 'NONE', #1382, #3212 ) ;
#5591=DIRECTION ( 'NONE',  ( -1.000000000000000000, -0.000000000000000000, -0.000000000000000000 ) ) ;
#5594=EDGE_CURVE ( 'NONE', #4559, #5270, #2642, .T. ) ;
#5595=CARTESIAN_POINT ( 'NONE',  ( 188.4942707396337482, 3.000000000000000000, 17.75098426722491851 ) ) ;
#5605=EDGE_CURVE ( 'NONE', #2502, #5312, #6694, .T. ) ;
#5607=DIRECTION ( 'NONE',  ( 0.000000000000000000, 1.000000000000000000, 0.000000000000000000 ) ) ;
#5609=CARTESIAN_POINT ( 'NONE',  ( 185.0000000000000000, -39.99999999999999289, 0.000000000000000000 ) ) ;
#5612=CIRCLE ( 'NONE', #7083, 2.999999999999999112 ) ;
#5615=CYLINDRICAL_SURFACE ( 'NONE', #1407, 3.000000000000000444 ) ;
#5619=VECTOR ( 'NONE', #6372, 1000.000000000000000 ) ;
#5620=CARTESIAN_POINT ( 'NONE',  ( 50.00000000000000000, -17.97033316447826579, 12.83599132585211322 ) ) ;
#5621=ORIENTED_EDGE ( 'NONE', *, *, #7463, .T. ) ;
#5622=DIRECTION ( 'NONE',  ( 0.000000000000000000, 0.000000000000000000, -1.000000000000000000 ) ) ;
#5626=CARTESIAN_POINT ( 'NONE',  ( 48.84364016120485275, 26.43524405526845200, 12.79091332731197461 ) ) ;
#5627=CARTESIAN_POINT ( 'NONE',  ( 217.0000000000000000, -9.000000000000001776, 18.00000000000001066 ) ) ;
#5631=CARTESIAN_POINT ( 'NONE',  ( 201.3397459621555470, -3.000000000000000888, 39.99999999999999289 ) ) ;
#5632=EDGE_CURVE ( 'NONE', #6935, #2502, #835, .T. ) ;
#5634=ORIENTED_EDGE ( 'NONE', *, *, #1376, .T. ) ;
#5639=CARTESIAN_POINT ( 'NONE',  ( 49.99999999999998579, -25.78715168812825098, 12.89530150989249435 ) ) ;
#5641=DIRECTION ( 'NONE',  ( 0.000000000000000000, -1.000000000000000000, 0.000000000000000000 ) ) ;
#5645=VERTEX_POINT ( 'NONE', #3149 ) ;
#5648=DIRECTION ( 'NONE',  ( 0.000000000000000000, -0.9860132971832693549, 0.1666666666666667684 ) ) ;
#5651=ADVANCED_FACE ( 'NONE', ( #4578 ), #6259, .F. ) ;
#5654=CIRCLE ( 'NONE', #2952, 6.000000000000019540 ) ;
#5656=DIRECTION ( 'NONE',  ( 0.000000000000000000, 0.000000000000000000, -1.000000000000000000 ) ) ;
#5661=VERTEX_POINT ( 'NONE', #487 ) ;
#5662=ADVANCED_FACE ( 'NONE', ( #3430 ), #5190, .F. ) ;
#5664=CYLINDRICAL_SURFACE ( 'NONE', #176, 3.000000000000000000 ) ;
#5669=DIRECTION ( 'NONE',  ( 0.4999999999999976685, 0.000000000000000000, 0.8660254037844400399 ) ) ;
#5679=DIRECTION ( 'NONE',  ( 1.000000000000000000, -0.000000000000000000, -0.000000000000000000 ) ) ;
#5680=CARTESIAN_POINT ( 'NONE',  ( 0.000000000000000000, 1.714505518806293455E-15, 21.00000000000001066 ) ) ;
#5681=LINE ( 'NONE', #404, #5831 ) ;
#5683=( BOUNDED_SURFACE ( )  B_SPLINE_SURFACE ( 3, 2, ( 
 ( #6125, #3204, #280 ),
 ( #2731, #4403, #1463 ),
 ( #849, #1537, #6741 ),
 ( #2622, #1497, #3861 ),
 ( #6195, #4224, #5626 ),
 ( #3901, #5087, #6569 ),
 ( #2010, #3652, #5992 ),
 ( #4944, #4369, #6854 ),
 ( #1083, #1660, #1574 ),
 ( #6275, #2893, #7009 ) ),
 .UNSPECIFIED., .F., .F., .T. ) 
 B_SPLINE_SURFACE_WITH_KNOTS ( ( 4, 2, 2, 2, 4 ),
 ( 3, 3 ),
 ( 0.000000000000000000, 0.3926990816987241395, 0.7853981633974482790, 1.178097245096172418, 1.570796326794896558 ),
 ( 0.000000000000000000, 1.000000000000000000 ),
 .UNSPECIFIED. ) 
 GEOMETRIC_REPRESENTATION_ITEM ( )  RATIONAL_B_SPLINE_SURFACE ( (
 ( 1.000000000000000000, 0.7372773368101256386, 1.000000000000000000),
 ( 1.000000000000000000, 0.7372805249393075133, 1.000000000000000000),
 ( 1.000000000000000000, 0.7365092403365430807, 1.000000000000000000),
 ( 1.000000000000000000, 0.7335393349597864043, 1.000000000000000000),
 ( 1.000000000000000000, 0.7313381170114944263, 1.000000000000000000),
 ( 1.000000000000000000, 0.7258018328328726954, 1.000000000000000000),
 ( 1.000000000000000000, 0.7224680490849620940, 1.000000000000000000),
 ( 1.000000000000000000, 0.7151362488948415086, 1.000000000000000000),
 ( 1.000000000000000000, 0.7111416486853837648, 1.000000000000000000),
 ( 1.000000000000000000, 0.7071067811865475727, 1.000000000000000000) ) ) 
 REPRESENTATION_ITEM ( '' )  SURFACE ( )  );
#5687=DIRECTION ( 'NONE',  ( 1.000000000000000000, -0.000000000000000000, -0.000000000000000000 ) ) ;
#5690=EDGE_CURVE ( 'NONE', #6366, #3365, #1638, .T. ) ;
#5691=CARTESIAN_POINT ( 'NONE',  ( 3.000000000000002665, -25.78715168812825098, 12.89530150989249435 ) ) ;
#5693=VERTEX_POINT ( 'NONE', #7411 ) ;
#5695=ADVANCED_FACE ( 'NONE', ( #2801 ), #7309, .T. ) ;
#5696=VERTEX_POINT ( 'NONE', #4457 ) ;
#5697=DIRECTION ( 'NONE',  ( -0.000000000000000000, -0.000000000000000000, 1.000000000000000000 ) ) ;
#5698=CARTESIAN_POINT ( 'NONE',  ( 53.00000000000000711, -20.99999999999999645, 10.00000000000000888 ) ) ;
#5699=ADVANCED_FACE ( 'NONE', ( #1563 ), #5805, .T. ) ;
#5703=CARTESIAN_POINT ( 'NONE',  ( 50.00000000000000000, 0.000000000000000000, 48.99999999999999289 ) ) ;
#5708=SPHERICAL_SURFACE ( 'NONE', #6762, 3.000000000000000000 ) ;
#5710=DIRECTION ( 'NONE',  ( 0.000000000000000000, -1.000000000000000000, -3.304235192336776498E-16 ) ) ;
#5712=EDGE_LOOP ( 'NONE', ( #5892, #1593, #3532, #3964, #5433, #1088, #474, #24 ) ) ;
#5713=EDGE_CURVE ( 'NONE', #6714, #5322, #5960, .T. ) ;
#5716=AXIS2_PLACEMENT_3D ( 'NONE', #2414, #3537, #1217 ) ;
#5719=DIRECTION ( 'NONE',  ( 0.000000000000000000, -0.9993908270190955401, 0.03489949670250346025 ) ) ;
#5725=LINE ( 'NONE', #4472, #785 ) ;
#5728=CARTESIAN_POINT ( 'NONE',  ( 47.00000000000000000, 30.03170604878415162, 10.00000000000001243 ) ) ;
#5729=CARTESIAN_POINT ( 'NONE',  ( 192.1021416551216419, -6.000000000000000888, 18.00000000000001066 ) ) ;
#5732=DIRECTION ( 'NONE',  ( -0.000000000000000000, -0.000000000000000000, 1.000000000000000000 ) ) ;
#5735=ORIENTED_EDGE ( 'NONE', *, *, #3912, .T. ) ;
#5738=FACE_BOUND ( 'NONE', #7492, .T. ) ;
#5739=VECTOR ( 'NONE', #641, 1000.000000000000000 ) ;
#5743=VERTEX_POINT ( 'NONE', #1685 ) ;
#5744=VECTOR ( 'NONE', #3094, 1000.000000000000000 ) ;
#5745=EDGE_CURVE ( 'NONE', #584, #3, #4617, .T. ) ;
#5747=CARTESIAN_POINT ( 'NONE',  ( 3.000000000000002665, -18.00000000000000000, 7.000000000000008882 ) ) ;
#5748=FACE_BOUND ( 'NONE', #4787, .T. ) ;
#5749=VERTEX_POINT ( 'NONE', #375 ) ;
#5750=AXIS2_PLACEMENT_3D ( 'NONE', #6466, #4701, #5812 ) ;
#5754=ORIENTED_EDGE ( 'NONE', *, *, #5562, .T. ) ;
#5755=VERTEX_POINT ( 'NONE', #5072 ) ;
#5757=CARTESIAN_POINT ( 'NONE',  ( 188.2878511289427195, 5.841022112857982229, 17.39345501382462444 ) ) ;
#5758=DIRECTION ( 'NONE',  ( -1.000000000000000000, 0.000000000000000000, 1.445602896647337931E-16 ) ) ;
#5764=DIRECTION ( 'NONE',  ( -1.000000000000000000, 0.000000000000000000, 0.000000000000000000 ) ) ;
#5765=DIRECTION ( 'NONE',  ( 0.000000000000000000, -1.000000000000000000, -1.836970198721029934E-16 ) ) ;
#5766=CARTESIAN_POINT ( 'NONE',  ( 0.000000000000000000, 24.05453786023368323, 12.47706554351403874 ) ) ;
#5767=EDGE_CURVE ( 'NONE', #6160, #3744, #2757, .T. ) ;
#5768=CARTESIAN_POINT ( 'NONE',  ( 3.000000000000000000, 21.91628335801839711, 36.91742634044857141 ) ) ;
#5769=CARTESIAN_POINT ( 'NONE',  ( 188.6380400399839061, -9.000000000000001776, 15.00000000000001066 ) ) ;
#5770=ORIENTED_EDGE ( 'NONE', *, *, #1487, .F. ) ;
#5771=ORIENTED_EDGE ( 'NONE', *, *, #3101, .F. ) ;
#5774=FACE_OUTER_BOUND ( 'NONE', #6502, .T. ) ;
#5776=CARTESIAN_POINT ( 'NONE',  ( 52.84383605861879829, -24.35311149449081825, 10.00000000000000888 ) ) ;
#5777=LINE ( 'NONE', #7085, #3119 ) ;
#5779=CIRCLE ( 'NONE', #2, 3.000000000000000888 ) ;
#5780=EDGE_LOOP ( 'NONE', ( #3433, #4172, #6425 ) ) ;
#5781=TOROIDAL_SURFACE ( 'NONE', #2459, 7.000000000000019540, 3.000000000000000000 ) ;
#5784=ORIENTED_EDGE ( 'NONE', *, *, #2353, .F. ) ;
#5786=EDGE_CURVE ( 'NONE', #2821, #3936, #426, .T. ) ;
#5787=CARTESIAN_POINT ( 'NONE',  ( 220.0000000000000000, 15.08392021690038121, 12.00000000000000711 ) ) ;
#5792=FACE_OUTER_BOUND ( 'NONE', #6552, .T. ) ;
#5794=CARTESIAN_POINT ( 'NONE',  ( 189.3200985330552726, 7.169359205023974724, 15.59067998186761095 ) ) ;
#5798=PLANE ( 'NONE',  #3933 ) ;
#5802=LINE ( 'NONE', #4615, #3120 ) ;
#5803=DIRECTION ( 'NONE',  ( 0.000000000000000000, 0.000000000000000000, 1.000000000000000000 ) ) ;
#5805=SPHERICAL_SURFACE ( 'NONE', #1655, 3.000000000000000000 ) ;
#5807=VECTOR ( 'NONE', #1603, 1000.000000000000000 ) ;
#5812=DIRECTION ( 'NONE',  ( -1.000000000000000000, 0.000000000000000000, 0.000000000000000000 ) ) ;
#5813=DIRECTION ( 'NONE',  ( -0.000000000000000000, -0.000000000000000000, 1.000000000000000000 ) ) ;
#5816=CARTESIAN_POINT ( 'NONE',  ( 217.0000000000000000, -56.99999999999999289, 3.000000000000000444 ) ) ;
#5820=DIRECTION ( 'NONE',  ( 0.000000000000000000, -1.000000000000000000, -2.065146995210484941E-16 ) ) ;
#5822=ORIENTED_EDGE ( 'NONE', *, *, #3382, .F. ) ;
#5824=CARTESIAN_POINT ( 'NONE',  ( 192.1021416551216419, -6.000000000000000000, 18.00000000000001066 ) ) ;
#5825=DIRECTION ( 'NONE',  ( -0.000000000000000000, 1.000000000000000000, 3.304235192336776498E-16 ) ) ;
#5826=CIRCLE ( 'NONE', #4470, 6.000000000000019540 ) ;
#5827=ORIENTED_EDGE ( 'NONE', *, *, #3200, .F. ) ;
#5831=VECTOR ( 'NONE', #3377, 1000.000000000000000 ) ;
#5836=LINE ( 'NONE', #558, #6638 ) ;
#5839=( GEOMETRIC_REPRESENTATION_CONTEXT ( 3 ) GLOBAL_UNCERTAINTY_ASSIGNED_CONTEXT ( ( #6144 ) ) GLOBAL_UNIT_ASSIGNED_CONTEXT ( ( #6028, #1945, #2023 ) ) REPRESENTATION_CONTEXT ( 'NONE', 'WORKASPACE' ) );
#5840=EDGE_CURVE ( 'NONE', #6366, #3524, #2083, .T. ) ;
#5843=LINE ( 'NONE', #5265, #151 ) ;
#5848=CARTESIAN_POINT ( 'NONE',  ( 209.9999999999999716, -6.000000000000000000, 35.00000000000000000 ) ) ;
#5851=ORIENTED_EDGE ( 'NONE', *, *, #5920, .F. ) ;
#5854=ORIENTED_EDGE ( 'NONE', *, *, #3641, .F. ) ;
#5862=ORIENTED_EDGE ( 'NONE', *, *, #2686, .T. ) ;
#5865=DIRECTION ( 'NONE',  ( -1.000000000000000000, 0.000000000000000000, -8.673617379884035472E-16 ) ) ;
#5866=DIRECTION ( 'NONE',  ( 1.000000000000000000, 0.000000000000000000, 0.000000000000000000 ) ) ;
#5867=CIRCLE ( 'NONE', #5496, 3.000000000000002665 ) ;
#5869=DIRECTION ( 'NONE',  ( -0.4999999999999976130, 0.000000000000000000, -0.8660254037844399289 ) ) ;
#5871=EDGE_CURVE ( 'NONE', #7205, #2384, #3656, .T. ) ;
#5875=ORIENTED_EDGE ( 'NONE', *, *, #7105, .T. ) ;
#5878=DIRECTION ( 'NONE',  ( -0.4999999999999950595, -0.000000000000000000, -0.8660254037844414832 ) ) ;
#5879=CARTESIAN_POINT ( 'NONE',  ( 188.9119595497369062, -5.725408222392992741, 18.47444250808088029 ) ) ;
#5880=EDGE_CURVE ( 'NONE', #6005, #722, #290, .T. ) ;
#5881=EDGE_CURVE ( 'NONE', #7091, #7026, #2263, .T. ) ;
#5883=ORIENTED_EDGE ( 'NONE', *, *, #7147, .T. ) ;
#5885=CARTESIAN_POINT ( 'NONE',  ( 192.1021416551216419, 6.000000000000000000, 18.00000000000001066 ) ) ;
#5886=ORIENTED_EDGE ( 'NONE', *, *, #5968, .T. ) ;
#5888=CYLINDRICAL_SURFACE ( 'NONE', #4765, 2.999999999999999112 ) ;
#5890=CYLINDRICAL_SURFACE ( 'NONE', #1527, 3.000000000000000000 ) ;
#5892=ORIENTED_EDGE ( 'NONE', *, *, #5871, .T. ) ;
#5898=VERTEX_POINT ( 'NONE', #5914 ) ;
#5899=EDGE_CURVE ( 'NONE', #4244, #6501, #5084, .T. ) ;
#5901=CARTESIAN_POINT ( 'NONE',  ( 217.0000000000000000, -56.99999999999999289, 3.000000000000000444 ) ) ;
#5902=AXIS2_PLACEMENT_3D ( 'NONE', #5609, #6291, #1018 ) ;
#5906=CARTESIAN_POINT ( 'NONE',  ( 188.6380400399839061, 9.000000000000001776, 15.00000000000000888 ) ) ;
#5907=AXIS2_PLACEMENT_3D ( 'NONE', #132, #663, #1933 ) ;
#5910=CARTESIAN_POINT ( 'NONE',  ( 220.0000000000000000, 18.00000000000000000, 7.000000000000008882 ) ) ;
#5914=CARTESIAN_POINT ( 'NONE',  ( 209.9999999999999716, -6.000000000000000000, 41.00000000000002132 ) ) ;
#5918=ORIENTED_EDGE ( 'NONE', *, *, #5899, .T. ) ;
#5919=ORIENTED_EDGE ( 'NONE', *, *, #1741, .T. ) ;
#5920=EDGE_CURVE ( 'NONE', #131, #1634, #3491, .T. ) ;
#5922=AXIS2_PLACEMENT_3D ( 'NONE', #836, #231, #2570 ) ;
#5923=CYLINDRICAL_SURFACE ( 'NONE', #7301, 3.000000000000000888 ) ;
#5932=CARTESIAN_POINT ( 'NONE',  ( 220.0000000000000000, 3.000000000000000000, 35.00000000000000000 ) ) ;
#5933=DIRECTION ( 'NONE',  ( 1.000000000000000000, 0.000000000000000000, 0.000000000000000000 ) ) ;
#5934=VERTEX_POINT ( 'NONE', #4414 ) ;
#5935=DIRECTION ( 'NONE',  ( 1.000000000000000000, 0.000000000000000000, 0.000000000000000000 ) ) ;
#5940=CIRCLE ( 'NONE', #2619, 8.500000000000007105 ) ;
#5941=( NAMED_UNIT ( * ) SI_UNIT ( $, .STERADIAN. ) SOLID_ANGLE_UNIT ( ) );
#5944=DIRECTION ( 'NONE',  ( -1.000000000000000000, 0.000000000000000000, 0.000000000000000000 ) ) ;
#5946=PRODUCT_DEFINITION_CONTEXT ( 'detailed design', #2693, 'design' ) ;
#5950=CARTESIAN_POINT ( 'NONE',  ( 217.0000000000000000, -56.99999999999999289, 0.000000000000000000 ) ) ;
#5952=DIRECTION ( 'NONE',  ( -0.8660254037844413721, 0.000000000000000000, 0.4999999999999950595 ) ) ;
#5954=AXIS2_PLACEMENT_3D ( 'NONE', #1692, #2885, #574 ) ;
#5957=AXIS2_PLACEMENT_3D ( 'NONE', #3959, #3387, #525 ) ;
#5959=EDGE_LOOP ( 'NONE', ( #6623, #5520, #5442, #1486 ) ) ;
#5960=CIRCLE ( 'NONE', #3635, 3.000000000000000888 ) ;
#5961=AXIS2_PLACEMENT_3D ( 'NONE', #6719, #791, #1444 ) ;
#5962=CARTESIAN_POINT ( 'NONE',  ( 217.0000000000000000, 6.000000000000000000, 18.00000000000001066 ) ) ;
#5968=EDGE_CURVE ( 'NONE', #529, #597, #6802, .T. ) ;
#5970=ORIENTED_EDGE ( 'NONE', *, *, #2161, .T. ) ;
#5976=DIRECTION ( 'NONE',  ( -0.000000000000000000, 1.000000000000000000, 0.000000000000000000 ) ) ;
#5980=VECTOR ( 'NONE', #5687, 1000.000000000000000 ) ;
#5982=CARTESIAN_POINT ( 'NONE',  ( 220.0000000000000000, 15.08392021690038121, 15.00000000000000888 ) ) ;
#5983=CARTESIAN_POINT ( 'NONE',  ( 217.0000000000000000, 56.99999999999999289, 3.000000000000021760 ) ) ;
#5984=CIRCLE ( 'NONE', #2175, 3.000000000000000000 ) ;
#5986=CYLINDRICAL_SURFACE ( 'NONE', #1238, 3.000000000000000000 ) ;
#5987=DIRECTION ( 'NONE',  ( 0.000000000000000000, -1.000000000000000000, -0.000000000000000000 ) ) ;
#5989=AXIS2_PLACEMENT_3D ( 'NONE', #4872, #137, #7207 ) ;
#5990=CARTESIAN_POINT ( 'NONE',  ( 0.000000000000000000, 0.000000000000000000, 48.99999999999999289 ) ) ;
#5992=CARTESIAN_POINT ( 'NONE',  ( 49.62135916575378047, 25.53693568588315799, 12.86832014125687884 ) ) ;
#5994=DIRECTION ( 'NONE',  ( -1.000000000000000000, 0.000000000000000000, 0.000000000000000000 ) ) ;
#5995=DIRECTION ( 'NONE',  ( 0.000000000000000000, 0.000000000000000000, -1.000000000000000000 ) ) ;
#5996=CARTESIAN_POINT ( 'NONE',  ( 189.0752568151670800, -7.489143060488414605, 15.37864083427403195 ) ) ;
#6000=CYLINDRICAL_SURFACE ( 'NONE', #5369, 2.999999999999999556 ) ;
#6003=CARTESIAN_POINT ( 'NONE',  ( 47.78524365475726654, -25.70892696317056192, 12.89802653137118860 ) ) ;
#6005=VERTEX_POINT ( 'NONE', #7445 ) ;
#6007=ADVANCED_FACE ( 'NONE', ( #2099 ), #107, .T. ) ;
#6015=EDGE_CURVE ( 'NONE', #5743, #4738, #4846, .T. ) ;
#6016=CARTESIAN_POINT ( 'NONE',  ( 0.000000000000000000, 0.000000000000000000, 35.00000000000000000 ) ) ;
#6019=CIRCLE ( 'NONE', #4964, 2.999999999999999112 ) ;
#6023=EDGE_LOOP ( 'NONE', ( #4279, #2283, #6048, #4314 ) ) ;
#6028=( LENGTH_UNIT ( ) NAMED_UNIT ( * ) SI_UNIT ( .MILLI., .METRE. ) );
#6029=CARTESIAN_POINT ( 'NONE',  ( 217.0000000000000000, 9.000000000000001776, 15.00000000000000888 ) ) ;
#6030=DIRECTION ( 'NONE',  ( 0.000000000000000000, -1.000000000000000000, 0.000000000000000000 ) ) ;
#6034=AXIS2_PLACEMENT_3D ( 'NONE', #1891, #3091, #3597 ) ;
#6035=ORIENTED_EDGE ( 'NONE', *, *, #5840, .F. ) ;
#6037=AXIS2_PLACEMENT_3D ( 'NONE', #2080, #3164, #5622 ) ;
#6038=DIRECTION ( 'NONE',  ( -0.000000000000000000, -0.000000000000000000, 1.000000000000000000 ) ) ;
#6039=DIRECTION ( 'NONE',  ( 0.000000000000000000, 0.000000000000000000, -1.000000000000000000 ) ) ;
#6041=DIRECTION ( 'NONE',  ( 0.000000000000000000, 0.000000000000000000, -1.000000000000000000 ) ) ;
#6045=ORIENTED_EDGE ( 'NONE', *, *, #3314, .T. ) ;
#6048=ORIENTED_EDGE ( 'NONE', *, *, #2603, .T. ) ;
#6057=DIRECTION ( 'NONE',  ( 1.000000000000000000, 0.000000000000000000, 0.000000000000000000 ) ) ;
#6058=CARTESIAN_POINT ( 'NONE',  ( 217.0000000000000000, 9.000000000000001776, 12.00000000000000711 ) ) ;
#6062=DIRECTION ( 'NONE',  ( -1.000000000000000000, 0.000000000000000000, 0.000000000000000000 ) ) ;
#6066=DIRECTION ( 'NONE',  ( 8.673617379884035472E-16, 0.000000000000000000, -1.000000000000000000 ) ) ;
#6071=CARTESIAN_POINT ( 'NONE',  ( 50.51471862576143224, -28.78532416918554304, 10.00000000000000711 ) ) ;
#6074=AXIS2_PLACEMENT_3D ( 'NONE', #2682, #3342, #7408 ) ;
#6075=VECTOR ( 'NONE', #3095, 1000.000000000000000 ) ;
#6077=CARTESIAN_POINT ( 'NONE',  ( 220.0000000000000000, -15.08392021690038121, 12.00000000000000711 ) ) ;
#6079=ORIENTED_EDGE ( 'NONE', *, *, #3575, .T. ) ;
#6082=EDGE_LOOP ( 'NONE', ( #5886, #6149, #5578, #3191 ) ) ;
#6087=AXIS2_PLACEMENT_3D ( 'NONE', #773, #6661, #3124 ) ;
#6091=ORIENTED_EDGE ( 'NONE', *, *, #1376, .F. ) ;
#6092=FACE_BOUND ( 'NONE', #6095, .T. ) ;
#6093=EDGE_CURVE ( 'NONE', #429, #1140, #3859, .T. ) ;
#6094=DIRECTION ( 'NONE',  ( 0.000000000000000000, 1.000000000000000000, -1.445602896647337931E-16 ) ) ;
#6095=EDGE_LOOP ( 'NONE', ( #2311, #3782 ) ) ;
#6096=EDGE_CURVE ( 'NONE', #1895, #4729, #5826, .T. ) ;
#6099=CIRCLE ( 'NONE', #444, 6.000000000000000000 ) ;
#6101=EDGE_CURVE ( 'NONE', #5513, #2163, #1147, .T. ) ;
#6102=DIRECTION ( 'NONE',  ( 1.000000000000000000, 0.000000000000000000, 0.000000000000000000 ) ) ;
#6111=VECTOR ( 'NONE', #2364, 1000.000000000000000 ) ;
#6112=CARTESIAN_POINT ( 'NONE',  ( 201.3397459621555470, 3.000000000000000000, 39.99999999999999289 ) ) ;
#6113=EDGE_CURVE ( 'NONE', #4244, #1140, #5802, .T. ) ;
#6117=ORIENTED_EDGE ( 'NONE', *, *, #6607, .T. ) ;
#6121=ORIENTED_EDGE ( 'NONE', *, *, #7175, .F. ) ;
#6123=FACE_OUTER_BOUND ( 'NONE', #6655, .T. ) ;
#6124=ORIENTED_EDGE ( 'NONE', *, *, #4411, .F. ) ;
#6125=CARTESIAN_POINT ( 'NONE',  ( 47.00000000000000000, 30.03170604878415162, 10.00000000000000888 ) ) ;
#6126=CARTESIAN_POINT ( 'NONE',  ( 47.00000000000000000, 27.04312195450891565, 12.73853277175702559 ) ) ;
#6132=EDGE_CURVE ( 'NONE', #2795, #7224, #780, .T. ) ;
#6133=ORIENTED_EDGE ( 'NONE', *, *, #6203, .F. ) ;
#6137=CARTESIAN_POINT ( 'NONE',  ( 188.1331788443806374, -8.454652614717035775, 15.00000000000001066 ) ) ;
#6140=ORIENTED_EDGE ( 'NONE', *, *, #571, .F. ) ;
#6141=DIRECTION ( 'NONE',  ( -0.000000000000000000, 1.000000000000000000, 0.000000000000000000 ) ) ;
#6144=UNCERTAINTY_MEASURE_WITH_UNIT (LENGTH_MEASURE( 1.000000000000000082E-05 ), #6028, 'distance_accuracy_value', 'NONE');
#6145=ORIENTED_EDGE ( 'NONE', *, *, #2515, .T. ) ;
#6146=EDGE_CURVE ( 'NONE', #233, #7468, #1596, .T. ) ;
#6149=ORIENTED_EDGE ( 'NONE', *, *, #4810, .F. ) ;
#6152=DIRECTION ( 'NONE',  ( 1.000000000000000000, 0.000000000000000000, 0.000000000000000000 ) ) ;
#6158=DIRECTION ( 'NONE',  ( 1.000000000000000000, -0.000000000000000000, -0.000000000000000000 ) ) ;
#6159=DIRECTION ( 'NONE',  ( 1.000000000000000000, 0.000000000000000000, 0.000000000000000000 ) ) ;
#6160=VERTEX_POINT ( 'NONE', #7373 ) ;
#6163=CARTESIAN_POINT ( 'NONE',  ( 185.0000000000000000, 39.99999999999999289, 0.000000000000000000 ) ) ;
#6166=EDGE_LOOP ( 'NONE', ( #3170, #884, #2910, #7261 ) ) ;
#6177=DIRECTION ( 'NONE',  ( -0.000000000000000000, -0.000000000000000000, 1.000000000000000000 ) ) ;
#6182=ORIENTED_EDGE ( 'NONE', *, *, #5302, .F. ) ;
#6184=EDGE_CURVE ( 'NONE', #2192, #597, #1641, .T. ) ;
#6186=ORIENTED_EDGE ( 'NONE', *, *, #1583, .F. ) ;
#6187=DIRECTION ( 'NONE',  ( 1.000000000000000000, 0.000000000000000000, 0.000000000000000000 ) ) ;
#6189=CIRCLE ( 'NONE', #300, 3.000000000000000000 ) ;
#6191=CIRCLE ( 'NONE', #1649, 22.00000000000000355 ) ;
#6192=ORIENTED_EDGE ( 'NONE', *, *, #4675, .T. ) ;
#6195=CARTESIAN_POINT ( 'NONE',  ( 50.68728032240937864, 28.82511565990200708, 10.00000000000000888 ) ) ;
#6197=CIRCLE ( 'NONE', #5961, 3.000000000000006217 ) ;
#6203=EDGE_CURVE ( 'NONE', #1231, #5033, #6806, .T. ) ;
#6204=CARTESIAN_POINT ( 'NONE',  ( 50.00000000000001421, -15.08392021690038121, 12.00000000000000711 ) ) ;
#6205=ORIENTED_EDGE ( 'NONE', *, *, #6864, .F. ) ;
#6206=VERTEX_POINT ( 'NONE', #2755 ) ;
#6211=CARTESIAN_POINT ( 'NONE',  ( 53.00000000000000711, 24.00878702352406435, 13.00000000000000888 ) ) ;
#6214=DIRECTION ( 'NONE',  ( -0.000000000000000000, -0.000000000000000000, 1.000000000000000000 ) ) ;
#6218=ORIENTED_EDGE ( 'NONE', *, *, #2603, .F. ) ;
#6224=VERTEX_POINT ( 'NONE', #5728 ) ;
#6231=CARTESIAN_POINT ( 'NONE',  ( 220.0000000000000000, 6.000000000000000000, 35.00000000000000000 ) ) ;
#6241=DIRECTION ( 'NONE',  ( 0.000000000000000000, 0.000000000000000000, -1.000000000000000000 ) ) ;
#6242=DIRECTION ( 'NONE',  ( 0.000000000000000000, 0.000000000000000000, 1.000000000000000000 ) ) ;
#6243=EDGE_LOOP ( 'NONE', ( #2194, #1820 ) ) ;
#6244=EDGE_LOOP ( 'NONE', ( #4278, #931, #3245, #986, #563, #6192 ) ) ;
#6246=LINE ( 'NONE', #3257, #2909 ) ;
#6248=CARTESIAN_POINT ( 'NONE',  ( 189.2277783884485132, 5.808582712248391289, 19.02145678267364559 ) ) ;
#6250=FACE_OUTER_BOUND ( 'NONE', #4574, .T. ) ;
#6251=DIRECTION ( 'NONE',  ( -0.000000000000000000, 1.000000000000000000, 0.000000000000000000 ) ) ;
#6259=PLANE ( 'NONE',  #4983 ) ;
#6266=VECTOR ( 'NONE', #4958, 1000.000000000000000 ) ;
#6267=CARTESIAN_POINT ( 'NONE',  ( 209.9999999999999716, -6.000000000000000000, 35.00000000000000000 ) ) ;
#6269=EDGE_CURVE ( 'NONE', #3365, #1652, #1658, .T. ) ;
#6272=CIRCLE ( 'NONE', #11, 2.999999999999999112 ) ;
#6273=VERTEX_POINT ( 'NONE', #1832 ) ;
#6275=CARTESIAN_POINT ( 'NONE',  ( 53.00000000000000000, 24.00878702352406435, 10.00000000000000888 ) ) ;
#6276=DIRECTION ( 'NONE',  ( 0.000000000000000000, 1.000000000000000000, 3.304235192336776498E-16 ) ) ;
#6278=ORIENTED_EDGE ( 'NONE', *, *, #5632, .T. ) ;
#6282=CARTESIAN_POINT ( 'NONE',  ( 43.50000000000001421, -39.99999999999999289, 10.00000000000000355 ) ) ;
#6289=EDGE_CURVE ( 'NONE', #5696, #5020, #1715, .T. ) ;
#6291=DIRECTION ( 'NONE',  ( -0.000000000000000000, -0.000000000000000000, 1.000000000000000000 ) ) ;
#6292=CARTESIAN_POINT ( 'NONE',  ( 50.00000000000000000, -22.78166690339260825, 13.00000000000000711 ) ) ;
#6295=AXIS2_PLACEMENT_3D ( 'NONE', #4891, #4458, #1485 ) ;
#6297=ORIENTED_EDGE ( 'NONE', *, *, #4043, .T. ) ;
#6300=DIRECTION ( 'NONE',  ( -0.000000000000000000, 0.000000000000000000, 1.000000000000000000 ) ) ;
#6301=DIRECTION ( 'NONE',  ( 0.000000000000000000, -0.000000000000000000, -1.000000000000000000 ) ) ;
#6302=CARTESIAN_POINT ( 'NONE',  ( 220.0000000000000000, -60.00000000000000000, 7.000000000000000888 ) ) ;
#6304=EDGE_CURVE ( 'NONE', #1997, #3892, #2389, .T. ) ;
#6309=AXIS2_PLACEMENT_3D ( 'NONE', #4597, #2126, #1087 ) ;
#6310=DIRECTION ( 'NONE',  ( 0.000000000000000000, 0.000000000000000000, -1.000000000000000000 ) ) ;
#6312=ORIENTED_EDGE ( 'NONE', *, *, #197, .F. ) ;
#6315=ORIENTED_EDGE ( 'NONE', *, *, #430, .T. ) ;
#6318=DIRECTION ( 'NONE',  ( 0.000000000000000000, 0.000000000000000000, -1.000000000000000000 ) ) ;
#6325=AXIS2_PLACEMENT_3D ( 'NONE', #5627, #2122, #6318 ) ;
#6327=ORIENTED_EDGE ( 'NONE', *, *, #7155, .F. ) ;
#6329=AXIS2_PLACEMENT_3D ( 'NONE', #301, #4390, #3734 ) ;
#6331=CIRCLE ( 'NONE', #3008, 8.500000000000007105 ) ;
#6332=CIRCLE ( 'NONE', #189, 3.000000000000004885 ) ;
#6336=FACE_OUTER_BOUND ( 'NONE', #2342, .T. ) ;
#6343=ADVANCED_FACE ( 'NONE', ( #4881 ), #1894, .T. ) ;
#6347=CARTESIAN_POINT ( 'NONE',  ( 201.3397459621555754, 3.000000000000000000, 39.99999999999997868 ) ) ;
#6351=MANIFOLD_SOLID_BREP ( 'Fillet2', #1968 ) ;
#6354=AXIS2_PLACEMENT_3D ( 'NONE', #2527, #180, #7217 ) ;
#6358=CARTESIAN_POINT ( 'NONE',  ( 53.00000000000000000, -22.78166690339260825, 10.00000000000000888 ) ) ;
#6360=ORIENTED_EDGE ( 'NONE', *, *, #3776, .T. ) ;
#6366=VERTEX_POINT ( 'NONE', #1014 ) ;
#6368=CYLINDRICAL_SURFACE ( 'NONE', #5537, 2.999999999999999112 ) ;
#6371=VERTEX_POINT ( 'NONE', #3258 ) ;
#6372=DIRECTION ( 'NONE',  ( 0.000000000000000000, 0.000000000000000000, -1.000000000000000000 ) ) ;
#6374=CARTESIAN_POINT ( 'NONE',  ( 189.5040654437683258, 6.000000000000000000, 19.50000000000000355 ) ) ;
#6381=DIRECTION ( 'NONE',  ( -0.000000000000000000, 1.000000000000000000, 1.836970198721029934E-16 ) ) ;
#6393=FACE_OUTER_BOUND ( 'NONE', #7584, .T. ) ;
#6403=CARTESIAN_POINT ( 'NONE',  ( 3.000000000000000000, -28.78532416918554304, 7.000000000000006217 ) ) ;
#6404=LINE ( 'NONE', #4794, #3971 ) ;
#6413=FACE_OUTER_BOUND ( 'NONE', #5120, .T. ) ;
#6419=CARTESIAN_POINT ( 'NONE',  ( 0.000000000000000000, 0.000000000000000000, 0.000000000000000000 ) ) ;
#6421=CARTESIAN_POINT ( 'NONE',  ( 188.0259799560787997, 8.302416934599655463, 15.00000000000000711 ) ) ;
#6425=ORIENTED_EDGE ( 'NONE', *, *, #7419, .F. ) ;
#6434=AXIS2_PLACEMENT_3D ( 'NONE', #1740, #1125, #2324 ) ;
#6435=EDGE_CURVE ( 'NONE', #2976, #6541, #6454, .T. ) ;
#6438=ORIENTED_EDGE ( 'NONE', *, *, #5745, .T. ) ;
#6443=AXIS2_PLACEMENT_3D ( 'NONE', #2265, #3885, #4038 ) ;
#6445=CARTESIAN_POINT ( 'NONE',  ( 50.00000000000000000, 17.97033316447826579, 12.83599132585211322 ) ) ;
#6446=VECTOR ( 'NONE', #3088, 1000.000000000000000 ) ;
#6447=AXIS2_PLACEMENT_3D ( 'NONE', #750, #1474, #7254 ) ;
#6451=CARTESIAN_POINT ( 'NONE',  ( 217.0000000000000000, -6.000000000000000000, 18.00000000000001066 ) ) ;
#6454=CIRCLE ( 'NONE', #6575, 3.000000000000002665 ) ;
#6456=ORIENTED_EDGE ( 'NONE', *, *, #2405, .F. ) ;
#6460=DIRECTION ( 'NONE',  ( -1.000000000000000000, -0.000000000000000000, -0.000000000000000000 ) ) ;
#6461=DIRECTION ( 'NONE',  ( 0.000000000000000000, 0.000000000000000000, 1.000000000000000000 ) ) ;
#6462=CIRCLE ( 'NONE', #1906, 25.00000000000000000 ) ;
#6464=ORIENTED_EDGE ( 'NONE', *, *, #1082, .F. ) ;
#6466=CARTESIAN_POINT ( 'NONE',  ( 3.000000000000000000, 56.99999999999999289, 7.000000000000022204 ) ) ;
#6467=DIRECTION ( 'NONE',  ( 0.000000000000000000, 0.000000000000000000, -1.000000000000000000 ) ) ;
#6470=CARTESIAN_POINT ( 'NONE',  ( 47.78553976602403708, -28.78532416918281456, 10.00000000000000533 ) ) ;
#6471=DIRECTION ( 'NONE',  ( -1.000000000000000000, 0.000000000000000000, 0.000000000000000000 ) ) ;
#6473=ORIENTED_EDGE ( 'NONE', *, *, #492, .F. ) ;
#6474=ORIENTED_EDGE ( 'NONE', *, *, #6435, .F. ) ;
#6476=CARTESIAN_POINT ( 'NONE',  ( 50.00000000000000000, -17.91234734164656928, 13.00000000000000888 ) ) ;
#6481=DIRECTION ( 'NONE',  ( 1.000000000000000000, 0.000000000000000000, 0.000000000000000000 ) ) ;
#6496=DIRECTION ( 'NONE',  ( 1.000000000000000000, 0.000000000000000000, -0.000000000000000000 ) ) ;
#6498=CARTESIAN_POINT ( 'NONE',  ( 50.00000000000000000, 18.00000000000000000, 15.00000000000000888 ) ) ;
#6500=EDGE_CURVE ( 'NONE', #7571, #5934, #3754, .T. ) ;
#6501=VERTEX_POINT ( 'NONE', #5371 ) ;
#6502=EDGE_LOOP ( 'NONE', ( #6920, #6988, #144, #4911 ) ) ;
#6505=DIRECTION ( 'NONE',  ( 1.000000000000000000, 0.000000000000000000, 0.000000000000000000 ) ) ;
#6506=EDGE_LOOP ( 'NONE', ( #3950, #6140, #3286, #482 ) ) ;
#6510=ORIENTED_EDGE ( 'NONE', *, *, #756, .T. ) ;
#6513=CARTESIAN_POINT ( 'NONE',  ( 50.00000000000000000, -24.54223912878477165, 12.93866904445501120 ) ) ;
#6518=AXIS2_PLACEMENT_3D ( 'NONE', #4103, #6057, #5329 ) ;
#6523=AXIS2_PLACEMENT_3D ( 'NONE', #4793, #4758, #5935 ) ;
#6527=DIRECTION ( 'NONE',  ( -0.000000000000000000, 1.000000000000000000, 3.304235192336776498E-16 ) ) ;
#6528=CARTESIAN_POINT ( 'NONE',  ( 209.9999999999999716, 3.000000000000000000, 35.00000000000000000 ) ) ;
#6530=VECTOR ( 'NONE', #7314, 1000.000000000000000 ) ;
#6531=CARTESIAN_POINT ( 'NONE',  ( 3.000000000000002665, 56.99999999999999289, 3.000000000000021760 ) ) ;
#6537=TOROIDAL_SURFACE ( 'NONE', #6037, 6.000000000000000000, 3.000000000000000000 ) ;
#6540=AXIS2_PLACEMENT_3D ( 'NONE', #6419, #1137, #3495 ) ;
#6541=VERTEX_POINT ( 'NONE', #4764 ) ;
#6542=VERTEX_POINT ( 'NONE', #4029 ) ;
#6543=CARTESIAN_POINT ( 'NONE',  ( 53.00000000000000711, -22.78166690339260825, 10.00000000000000711 ) ) ;
#6550=FACE_OUTER_BOUND ( 'NONE', #6506, .T. ) ;
#6552=EDGE_LOOP ( 'NONE', ( #4133, #4081, #6315, #3021, #7450, #7096, #7130, #4993, #6145, #3090 ) ) ;
#6557=DIRECTION ( 'NONE',  ( 0.000000000000000000, 0.000000000000000000, 1.000000000000000000 ) ) ;
#6565=VECTOR ( 'NONE', #2546, 1000.000000000000114 ) ;
#6569=CARTESIAN_POINT ( 'NONE',  ( 49.39900052591443114, 25.87352760396088058, 12.83931617239071166 ) ) ;
#6570=DIRECTION ( 'NONE',  ( 1.000000000000000000, 0.000000000000000000, 0.000000000000000000 ) ) ;
#6573=CARTESIAN_POINT ( 'NONE',  ( 186.1301251221888720, -7.429512690641201011, 13.65616394131904343 ) ) ;
#6575=AXIS2_PLACEMENT_3D ( 'NONE', #3874, #1747, #5325 ) ;
#6581=DIRECTION ( 'NONE',  ( -0.000000000000000000, -0.000000000000000000, -1.000000000000000000 ) ) ;
#6592=CARTESIAN_POINT ( 'NONE',  ( 220.0000000000000000, 56.99999999999999289, 7.000000000000022204 ) ) ;
#6594=ORIENTED_EDGE ( 'NONE', *, *, #1457, .T. ) ;
#6603=VECTOR ( 'NONE', #3450, 1000.000000000000000 ) ;
#6604=SPHERICAL_SURFACE ( 'NONE', #6354, 3.000000000000000000 ) ;
#6607=EDGE_CURVE ( 'NONE', #3543, #7465, #3279, .T. ) ;
#6612=ORIENTED_EDGE ( 'NONE', *, *, #6093, .F. ) ;
#6614=CARTESIAN_POINT ( 'NONE',  ( 43.50000000000001421, -39.99999999999999289, 0.000000000000000000 ) ) ;
#6621=FACE_OUTER_BOUND ( 'NONE', #2733, .T. ) ;
#6623=ORIENTED_EDGE ( 'NONE', *, *, #4102, .F. ) ;
#6628=CARTESIAN_POINT ( 'NONE',  ( 192.1021416551216419, -3.000000000000000000, 18.00000000000001421 ) ) ;
#6629=DIRECTION ( 'NONE',  ( 0.000000000000000000, 1.000000000000000000, 0.000000000000000000 ) ) ;
#6638=VECTOR ( 'NONE', #2906, 1000.000000000000000 ) ;
#6644=DIRECTION ( 'NONE',  ( 1.000000000000000000, -0.000000000000000000, -0.000000000000000000 ) ) ;
#6651=DIRECTION ( 'NONE',  ( 0.000000000000000000, 0.000000000000000000, -1.000000000000000000 ) ) ;
#6654=EDGE_CURVE ( 'NONE', #7538, #7239, #6331, .T. ) ;
#6655=EDGE_LOOP ( 'NONE', ( #7343, #1506, #3134, #3059, #2946, #371, #5875, #5634, #3117, #416, #1109, #4791, #3928, #3592 ) ) ;
#6659=ORIENTED_EDGE ( 'NONE', *, *, #6113, .T. ) ;
#6661=DIRECTION ( 'NONE',  ( -0.000000000000000000, -1.000000000000000000, -0.000000000000000000 ) ) ;
#6663=ORIENTED_EDGE ( 'NONE', *, *, #54, .T. ) ;
#6666=DIRECTION ( 'NONE',  ( 0.000000000000000000, -1.445602896647337931E-16, -1.000000000000000000 ) ) ;
#6670=FACE_OUTER_BOUND ( 'NONE', #4505, .T. ) ;
#6673=ADVANCED_FACE ( 'NONE', ( #7209 ), #139, .T. ) ;
#6676=CARTESIAN_POINT ( 'NONE',  ( 0.000000000000000000, -56.99999999999999289, 0.000000000000000000 ) ) ;
#6678=CARTESIAN_POINT ( 'NONE',  ( 217.0000000000000000, -15.08392021690038121, 12.00000000000000711 ) ) ;
#6684=ORIENTED_EDGE ( 'NONE', *, *, #713, .F. ) ;
#6694=CIRCLE ( 'NONE', #6329, 3.000000000000000000 ) ;
#6695=CIRCLE ( 'NONE', #6818, 2.999999999999999112 ) ;
#6696=VERTEX_POINT ( 'NONE', #1353 ) ;
#6704=ORIENTED_EDGE ( 'NONE', *, *, #7463, .F. ) ;
#6707=CYLINDRICAL_SURFACE ( 'NONE', #2141, 8.500000000000007105 ) ;
#6709=CYLINDRICAL_SURFACE ( 'NONE', #2845, 25.00000000000000000 ) ;
#6710=DIRECTION ( 'NONE',  ( 1.000000000000000000, 0.000000000000000000, 0.000000000000000000 ) ) ;
#6714=VERTEX_POINT ( 'NONE', #5555 ) ;
#6716=AXIS2_PLACEMENT_3D ( 'NONE', #221, #7253, #2022 ) ;
#6719=CARTESIAN_POINT ( 'NONE',  ( 192.1021416551216419, 3.000000000000000000, 18.00000000000001421 ) ) ;
#6721=DIRECTION ( 'NONE',  ( -1.000000000000000000, 0.000000000000000000, -0.000000000000000000 ) ) ;
#6722=CARTESIAN_POINT ( 'NONE',  ( 217.0000000000000000, -56.99999999999999289, 7.000000000000000888 ) ) ;
#6726=VERTEX_POINT ( 'NONE', #5519 ) ;
#6734=LINE ( 'NONE', #5043, #6565 ) ;
#6737=FACE_OUTER_BOUND ( 'NONE', #6082, .T. ) ;
#6739=EDGE_CURVE ( 'NONE', #5563, #2614, #3992, .T. ) ;
#6740=DIRECTION ( 'NONE',  ( -1.000000000000000000, -0.000000000000000000, -0.000000000000000000 ) ) ;
#6741=CARTESIAN_POINT ( 'NONE',  ( 47.78524365475804103, 26.96414633745969525, 12.74533806390693691 ) ) ;
#6742=DIRECTION ( 'NONE',  ( 0.000000000000000000, 0.000000000000000000, 1.000000000000000000 ) ) ;
#6744=CARTESIAN_POINT ( 'NONE',  ( 0.000000000000000000, -2.312964634635744633E-15, 7.000000000000002665 ) ) ;
#6747=EDGE_LOOP ( 'NONE', ( #305, #6464, #3827, #2223 ) ) ;
#6748=EDGE_CURVE ( 'NONE', #3993, #584, #6191, .T. ) ;
#6749=DIRECTION ( 'NONE',  ( 1.000000000000000000, 0.000000000000000000, 0.000000000000000000 ) ) ;
#6751=DIRECTION ( 'NONE',  ( 0.000000000000000000, 0.000000000000000000, -1.000000000000000000 ) ) ;
#6753=ORIENTED_EDGE ( 'NONE', *, *, #207, .T. ) ;
#6754=CARTESIAN_POINT ( 'NONE',  ( 3.000000000000002665, -56.99999999999999289, 7.000000000000000000 ) ) ;
#6755=VECTOR ( 'NONE', #5679, 1000.000000000000000 ) ;
#6758=EDGE_CURVE ( 'NONE', #2192, #2574, #2011, .T. ) ;
#6759=ORIENTED_EDGE ( 'NONE', *, *, #7175, .T. ) ;
#6760=LINE ( 'NONE', #6840, #7206 ) ;
#6762=AXIS2_PLACEMENT_3D ( 'NONE', #5206, #7509, #5865 ) ;
#6767=ADVANCED_FACE ( 'NONE', ( #4370 ), #6707, .F. ) ;
#6770=ORIENTED_EDGE ( 'NONE', *, *, #4949, .F. ) ;
#6772=CARTESIAN_POINT ( 'NONE',  ( 217.0000000000000000, 15.08392021690037943, 12.00000000000000711 ) ) ;
#6773=CARTESIAN_POINT ( 'NONE',  ( 35.00000000000000000, -39.99999999999999289, 10.00000000000000355 ) ) ;
#6775=CIRCLE ( 'NONE', #3835, 8.500000000000007105 ) ;
#6776=ADVANCED_FACE ( 'NONE', ( #3902 ), #4612, .T. ) ;
#6777=CARTESIAN_POINT ( 'NONE',  ( 209.9999999999999716, 6.000000000000000000, 28.99999999999998579 ) ) ;
#6778=DIRECTION ( 'NONE',  ( 0.000000000000000000, 0.000000000000000000, 1.000000000000000000 ) ) ;
#6782=CIRCLE ( 'NONE', #6903, 3.000000000000001332 ) ;
#6783=CARTESIAN_POINT ( 'NONE',  ( 47.00000000000000000, -24.98477067547739239, 35.87248741756260983 ) ) ;
#6784=DIRECTION ( 'NONE',  ( -0.000000000000000000, -0.000000000000000000, 1.000000000000000000 ) ) ;
#6791=CARTESIAN_POINT ( 'NONE',  ( 186.9025342811887924, 8.510922567869524613, 14.99401584891889172 ) ) ;
#6793=CARTESIAN_POINT ( 'NONE',  ( 50.00000000000000000, 0.000000000000000000, 35.00000000000000000 ) ) ;
#6797=ORIENTED_EDGE ( 'NONE', *, *, #7525, .F. ) ;
#6802=CIRCLE ( 'NONE', #5459, 3.000000000000002665 ) ;
#6805=VECTOR ( 'NONE', #2813, 1000.000000000000000 ) ;
#6806=CIRCLE ( 'NONE', #7297, 8.500000000000007105 ) ;
#6812=CIRCLE ( 'NONE', #2751, 2.999999999999999112 ) ;
#6814=ADVANCED_FACE ( 'NONE', ( #5748, #3405, #3974 ), #3244, .F. ) ;
#6818=AXIS2_PLACEMENT_3D ( 'NONE', #2062, #292, #6751 ) ;
#6825=EDGE_CURVE ( 'NONE', #797, #7571, #7422, .T. ) ;
#6828=DIRECTION ( 'NONE',  ( -0.000000000000000000, 1.000000000000000000, 1.836970198721029934E-16 ) ) ;
#6830=CARTESIAN_POINT ( 'NONE',  ( 50.00000000000000000, 24.00878702352406435, 13.00000000000000888 ) ) ;
#6836=AXIS2_PLACEMENT_3D ( 'NONE', #3536, #6496, #2798 ) ;
#6840=CARTESIAN_POINT ( 'NONE',  ( 209.9999999999999716, 6.000000000000000000, 28.99999999999998934 ) ) ;
#6842=LINE ( 'NONE', #6302, #4580 ) ;
#6845=ORIENTED_EDGE ( 'NONE', *, *, #1814, .T. ) ;
#6846=AXIS2_PLACEMENT_3D ( 'NONE', #5901, #4796, #7131 ) ;
#6854=CARTESIAN_POINT ( 'NONE',  ( 49.92191802931394307, 24.80301777383411022, 12.93156150603311083 ) ) ;
#6861=EDGE_LOOP ( 'NONE', ( #4953, #6845, #310 ) ) ;
#6863=CARTESIAN_POINT ( 'NONE',  ( 220.0000000000000000, -3.000000000000000000, 0.000000000000000000 ) ) ;
#6864=EDGE_CURVE ( 'NONE', #1604, #258, #1035, .T. ) ;
#6867=CARTESIAN_POINT ( 'NONE',  ( 187.7498399038581454, 3.766229566949281349, 16.46159223694064622 ) ) ;
#6873=EDGE_LOOP ( 'NONE', ( #5481, #7149, #7442, #3141, #6684 ) ) ;
#6885=ORIENTED_EDGE ( 'NONE', *, *, #571, .T. ) ;
#6886=CARTESIAN_POINT ( 'NONE',  ( 217.0000000000000000, -6.000000000000000000, 35.00000000000000000 ) ) ;
#6888=VECTOR ( 'NONE', #4407, 1000.000000000000000 ) ;
#6892=DIRECTION ( 'NONE',  ( 0.000000000000000000, 0.000000000000000000, -1.000000000000000000 ) ) ;
#6893=ORIENTED_EDGE ( 'NONE', *, *, #7307, .F. ) ;
#6897=DIRECTION ( 'NONE',  ( -0.000000000000000000, 1.000000000000000000, 0.000000000000000000 ) ) ;
#6898=CIRCLE ( 'NONE', #7511, 3.000000000000000000 ) ;
#6900=EDGE_LOOP ( 'NONE', ( #3757, #4545, #746, #6972 ) ) ;
#6902=DIRECTION ( 'NONE',  ( -1.000000000000000000, 0.000000000000000000, -0.000000000000000000 ) ) ;
#6903=AXIS2_PLACEMENT_3D ( 'NONE', #5168, #437, #933 ) ;
#6905=CARTESIAN_POINT ( 'NONE',  ( 188.9082403859883073, 5.724479639934364705, 18.46800072750736987 ) ) ;
#6911=ORIENTED_EDGE ( 'NONE', *, *, #1275, .F. ) ;
#6912=ORIENTED_EDGE ( 'NONE', *, *, #3963, .F. ) ;
#6913=DIRECTION ( 'NONE',  ( 0.000000000000000000, 0.000000000000000000, 1.000000000000000000 ) ) ;
#6914=FACE_BOUND ( 'NONE', #3858, .T. ) ;
#6915=FACE_OUTER_BOUND ( 'NONE', #6023, .T. ) ;
#6916=CARTESIAN_POINT ( 'NONE',  ( 50.00000000000000000, 24.90486745229362953, 37.17889356869155648 ) ) ;
#6918=ADVANCED_FACE ( 'NONE', ( #1575 ), #4090, .T. ) ;
#6919=ORIENTED_EDGE ( 'NONE', *, *, #3322, .F. ) ;
#6920=ORIENTED_EDGE ( 'NONE', *, *, #3814, .T. ) ;
#6928=CYLINDRICAL_SURFACE ( 'NONE', #6945, 3.000000000000000888 ) ;
#6932=ORIENTED_EDGE ( 'NONE', *, *, #6739, .F. ) ;
#6935=VERTEX_POINT ( 'NONE', #1777 ) ;
#6940=AXIS2_PLACEMENT_3D ( 'NONE', #7526, #2267, #2613 ) ;
#6941=LINE ( 'NONE', #7440, #658 ) ;
#6942=VERTEX_POINT ( 'NONE', #5281 ) ;
#6944=AXIS2_PLACEMENT_3D ( 'NONE', #1372, #2537, #6039 ) ;
#6945=AXIS2_PLACEMENT_3D ( 'NONE', #2692, #3818, #4512 ) ;
#6959=CARTESIAN_POINT ( 'NONE',  ( 220.0000000000000000, 56.99999999999999289, 10.00000000000002309 ) ) ;
#6960=DIRECTION ( 'NONE',  ( 0.000000000000000000, 0.9961946980917452121, 0.08715574274766277330 ) ) ;
#6966=AXIS2_PLACEMENT_3D ( 'NONE', #358, #3911, #3214 ) ;
#6970=CARTESIAN_POINT ( 'NONE',  ( 49.45068872151877315, -24.66606923277885599, 10.00000000000000178 ) ) ;
#6971=CARTESIAN_POINT ( 'NONE',  ( 3.000000000000002665, 30.03170604878415162, 10.00000000000001243 ) ) ;
#6972=ORIENTED_EDGE ( 'NONE', *, *, #2802, .F. ) ;
#6980=ORIENTED_EDGE ( 'NONE', *, *, #3135, .F. ) ;
#6981=EDGE_LOOP ( 'NONE', ( #7503, #1985, #6994, #6091 ) ) ;
#6988=ORIENTED_EDGE ( 'NONE', *, *, #865, .T. ) ;
#6994=ORIENTED_EDGE ( 'NONE', *, *, #4623, .F. ) ;
#6998=ORIENTED_EDGE ( 'NONE', *, *, #911, .F. ) ;
#7000=CARTESIAN_POINT ( 'NONE',  ( 49.99999999999999289, -23.17515487249191963, 12.98629252876240514 ) ) ;
#7002=ORIENTED_EDGE ( 'NONE', *, *, #713, .T. ) ;
#7003=AXIS2_PLACEMENT_3D ( 'NONE', #6793, #945, #3297 ) ;
#7009=CARTESIAN_POINT ( 'NONE',  ( 49.99999999999999289, 24.00878702352406435, 13.00000000000000711 ) ) ;
#7016=ORIENTED_EDGE ( 'NONE', *, *, #3702, .F. ) ;
#7018=AXIS2_PLACEMENT_3D ( 'NONE', #5479, #703, #7128 ) ;
#7023=CYLINDRICAL_SURFACE ( 'NONE', #6518, 2.999999999999999112 ) ;
#7026=VERTEX_POINT ( 'NONE', #5766 ) ;
#7029=DIRECTION ( 'NONE',  ( 0.000000000000000000, 1.000000000000000000, 0.000000000000000000 ) ) ;
#7035=ORIENTED_EDGE ( 'NONE', *, *, #4623, .T. ) ;
#7037=ADVANCED_FACE ( 'NONE', ( #6915 ), #7410, .F. ) ;
#7038=FACE_OUTER_BOUND ( 'NONE', #4012, .T. ) ;
#7039=EDGE_LOOP ( 'NONE', ( #3056, #1854, #3632, #3050 ) ) ;
#7044=DIRECTION ( 'NONE',  ( 0.000000000000000000, -0.08715574274766212104, 0.9961946980917452121 ) ) ;
#7052=AXIS2_PLACEMENT_3D ( 'NONE', #565, #5878, #5952 ) ;
#7053=ORIENTED_EDGE ( 'NONE', *, *, #3641, .T. ) ;
#7063=CARTESIAN_POINT ( 'NONE',  ( 0.000000000000000000, -1.445602896647342072E-15, 7.000000000000012434 ) ) ;
#7064=AXIS2_PLACEMENT_3D ( 'NONE', #2759, #6301, #4541 ) ;
#7069=SPHERICAL_SURFACE ( 'NONE', #85, 3.000000000000000000 ) ;
#7070=CARTESIAN_POINT ( 'NONE',  ( 203.9378221735088630, 3.000000000000000000, 38.49999999999999289 ) ) ;
#7071=DIRECTION ( 'NONE',  ( 0.000000000000000000, -1.000000000000000000, 0.000000000000000000 ) ) ;
#7072=AXIS2_PLACEMENT_3D ( 'NONE', #1813, #87, #1654 ) ;
#7075=ORIENTED_EDGE ( 'NONE', *, *, #6500, .T. ) ;
#7079=CARTESIAN_POINT ( 'NONE',  ( 3.000000000000000000, -56.99999999999999289, 7.000000000000000888 ) ) ;
#7081=ORIENTED_EDGE ( 'NONE', *, *, #4286, .T. ) ;
#7083=AXIS2_PLACEMENT_3D ( 'NONE', #5462, #2536, #4306 ) ;
#7085=CARTESIAN_POINT ( 'NONE',  ( 50.00000000000000000, 0.000000000000000000, 60.00000000000000711 ) ) ;
#7086=ORIENTED_EDGE ( 'NONE', *, *, #6015, .F. ) ;
#7087=ORIENTED_EDGE ( 'NONE', *, *, #4995, .T. ) ;
#7091=VERTEX_POINT ( 'NONE', #3429 ) ;
#7093=DIRECTION ( 'NONE',  ( 0.000000000000000000, 0.000000000000000000, 1.000000000000000000 ) ) ;
#7096=ORIENTED_EDGE ( 'NONE', *, *, #5690, .F. ) ;
#7102=DIRECTION ( 'NONE',  ( 1.000000000000000000, 0.000000000000000000, 0.000000000000000000 ) ) ;
#7103=CYLINDRICAL_SURFACE ( 'NONE', #4059, 3.000000000000000000 ) ;
#7105=EDGE_CURVE ( 'NONE', #529, #5743, #1684, .T. ) ;
#7108=FACE_OUTER_BOUND ( 'NONE', #5780, .T. ) ;
#7109=CARTESIAN_POINT ( 'NONE',  ( 186.9059892324150383, -5.031373033403107264, 15.00000000000000888 ) ) ;
#7115=EDGE_LOOP ( 'NONE', ( #335, #4967, #7053, #4704, #5621 ) ) ;
#7118=ORIENTED_EDGE ( 'NONE', *, *, #197, .T. ) ;
#7128=DIRECTION ( 'NONE',  ( 0.000000000000000000, 0.000000000000000000, -1.000000000000000000 ) ) ;
#7129=DIRECTION ( 'NONE',  ( -1.000000000000000000, 0.000000000000000000, -0.000000000000000000 ) ) ;
#7130=ORIENTED_EDGE ( 'NONE', *, *, #5840, .T. ) ;
#7131=DIRECTION ( 'NONE',  ( 0.000000000000000000, 0.000000000000000000, -1.000000000000000000 ) ) ;
#7133=CARTESIAN_POINT ( 'NONE',  ( 50.00000000000000000, 24.00878702352406435, 13.00000000000000888 ) ) ;
#7137=CARTESIAN_POINT ( 'NONE',  ( 176.5000000000000000, 39.99999999999999289, 0.000000000000000000 ) ) ;
#7144=CARTESIAN_POINT ( 'NONE',  ( 188.1399229816385628, 8.449061396769250720, 15.00000000000000888 ) ) ;
#7146=CARTESIAN_POINT ( 'NONE',  ( 186.9827202257732779, -7.949242328481256337, 15.13290197900971634 ) ) ;
#7147=EDGE_CURVE ( 'NONE', #1634, #496, #2836, .T. ) ;
#7149=ORIENTED_EDGE ( 'NONE', *, *, #7238, .F. ) ;
#7155=EDGE_CURVE ( 'NONE', #7026, #5645, #2021, .T. ) ;
#7157=EDGE_CURVE ( 'NONE', #5755, #5359, #3880, .T. ) ;
#7158=EDGE_LOOP ( 'NONE', ( #6205, #6218 ) ) ;
#7163=FACE_OUTER_BOUND ( 'NONE', #5712, .T. ) ;
#7165=ORIENTED_EDGE ( 'NONE', *, *, #3720, .F. ) ;
#7169=CARTESIAN_POINT ( 'NONE',  ( 3.000000000000000000, -21.98659819442010388, 35.76778892745510063 ) ) ;
#7175=EDGE_CURVE ( 'NONE', #2821, #647, #27, .T. ) ;
#7176=AXIS2_PLACEMENT_3D ( 'NONE', #484, #2144, #4498 ) ;
#7181=CARTESIAN_POINT ( 'NONE',  ( 189.9732893686090449, -6.600999473907240400, 16.15635983897348282 ) ) ;
#7188=AXIS2_PLACEMENT_3D ( 'NONE', #1892, #812, #4284 ) ;
#7189=ADVANCED_FACE ( 'NONE', ( #2486 ), #73, .F. ) ;
#7197=ORIENTED_EDGE ( 'NONE', *, *, #6289, .F. ) ;
#7198=EDGE_CURVE ( 'NONE', #1310, #3769, #3390, .T. ) ;
#7201=VERTEX_POINT ( 'NONE', #4226 ) ;
#7205=VERTEX_POINT ( 'NONE', #564 ) ;
#7206=VECTOR ( 'NONE', #7300, 1000.000000000000000 ) ;
#7207=DIRECTION ( 'NONE',  ( 0.000000000000000000, 0.000000000000000000, -1.000000000000000000 ) ) ;
#7209=FACE_OUTER_BOUND ( 'NONE', #541, .T. ) ;
#7210=ORIENTED_EDGE ( 'NONE', *, *, #909, .F. ) ;
#7215=ORIENTED_EDGE ( 'NONE', *, *, #2213, .T. ) ;
#7217=DIRECTION ( 'NONE',  ( -1.000000000000000000, 0.000000000000000000, 0.000000000000000000 ) ) ;
#7222=EDGE_CURVE ( 'NONE', #5579, #6726, #6332, .T. ) ;
#7224=VERTEX_POINT ( 'NONE', #4191 ) ;
#7227=CARTESIAN_POINT ( 'NONE',  ( 220.0000000000000000, -20.99999999999999645, 13.00000000000000888 ) ) ;
#7229=DIRECTION ( 'NONE',  ( 1.000000000000000000, 0.000000000000000000, 0.000000000000000000 ) ) ;
#7230=ORIENTED_EDGE ( 'NONE', *, *, #3797, .T. ) ;
#7231=EDGE_LOOP ( 'NONE', ( #6456, #2455, #996, #4513 ) ) ;
#7235=CARTESIAN_POINT ( 'NONE',  ( 217.0000000000000000, 15.08392021690037943, 12.00000000000000711 ) ) ;
#7238=EDGE_CURVE ( 'NONE', #510, #7201, #3263, .T. ) ;
#7239=VERTEX_POINT ( 'NONE', #1179 ) ;
#7241=CARTESIAN_POINT ( 'NONE',  ( 50.00000000000000000, 25.78625927331255951, 12.84683604381136668 ) ) ;
#7242=ORIENTED_EDGE ( 'NONE', *, *, #124, .T. ) ;
#7249=EDGE_LOOP ( 'NONE', ( #7461, #1837 ) ) ;
#7253=DIRECTION ( 'NONE',  ( 0.000000000000000000, 0.000000000000000000, 1.000000000000000000 ) ) ;
#7254=DIRECTION ( 'NONE',  ( 1.000000000000000000, 0.000000000000000000, 0.000000000000000000 ) ) ;
#7261=ORIENTED_EDGE ( 'NONE', *, *, #2161, .F. ) ;
#7265=LINE ( 'NONE', #6614, #1398 ) ;
#7270=ORIENTED_EDGE ( 'NONE', *, *, #1082, .T. ) ;
#7275=FACE_OUTER_BOUND ( 'NONE', #3778, .T. ) ;
#7276=CARTESIAN_POINT ( 'NONE',  ( 209.9999999999999716, 6.000000000000000000, 35.00000000000000000 ) ) ;
#7278=CARTESIAN_POINT ( 'NONE',  ( 220.0000000000000000, -18.04196010845019060, 12.50000000000000711 ) ) ;
#7286=CARTESIAN_POINT ( 'NONE',  ( 201.3397459621555470, 6.000000000000000000, 39.99999999999999289 ) ) ;
#7288=DIRECTION ( 'NONE',  ( 0.000000000000000000, 0.000000000000000000, 1.000000000000000000 ) ) ;
#7293=DIRECTION ( 'NONE',  ( 0.000000000000000000, 0.000000000000000000, 1.000000000000000000 ) ) ;
#7296=VECTOR ( 'NONE', #7044, 1000.000000000000000 ) ;
#7297=AXIS2_PLACEMENT_3D ( 'NONE', #7451, #988, #408 ) ;
#7298=ORIENTED_EDGE ( 'NONE', *, *, #7361, .F. ) ;
#7299=ORIENTED_EDGE ( 'NONE', *, *, #5163, .F. ) ;
#7300=DIRECTION ( 'NONE',  ( -0.000000000000000000, -1.000000000000000000, -0.000000000000000000 ) ) ;
#7301=AXIS2_PLACEMENT_3D ( 'NONE', #82, #3663, #3621 ) ;
#7302=DIRECTION ( 'NONE',  ( 0.000000000000000000, 0.000000000000000000, -1.000000000000000000 ) ) ;
#7307=EDGE_CURVE ( 'NONE', #2574, #4244, #5266, .T. ) ;
#7309=TOROIDAL_SURFACE ( 'NONE', #3997, 6.000000000000000000, 3.000000000000000000 ) ;
#7311=ORIENTED_EDGE ( 'NONE', *, *, #3447, .F. ) ;
#7312=CARTESIAN_POINT ( 'NONE',  ( 50.04196010845020481, 18.04196010845019060, 12.50000000000000711 ) ) ;
#7314=DIRECTION ( 'NONE',  ( 0.000000000000000000, -1.000000000000000000, -1.836970198721029934E-16 ) ) ;
#7320=CARTESIAN_POINT ( 'NONE',  ( 186.9059892324150383, 5.031373033403108153, 15.00000000000000888 ) ) ;
#7321=CARTESIAN_POINT ( 'NONE',  ( 220.0000000000000000, 60.00000000000000000, 10.00000000000002309 ) ) ;
#7331=LINE ( 'NONE', #4410, #1311 ) ;
#7332=CARTESIAN_POINT ( 'NONE',  ( 3.000000000000002665, -28.78532416918554304, 10.00000000000000711 ) ) ;
#7335=LINE ( 'NONE', #2027, #4 ) ;
#7341=DIRECTION ( 'NONE',  ( 1.000000000000000000, 0.000000000000000000, 0.000000000000000000 ) ) ;
#7342=DIRECTION ( 'NONE',  ( 0.000000000000000000, 0.000000000000000000, -1.000000000000000000 ) ) ;
#7343=ORIENTED_EDGE ( 'NONE', *, *, #5374, .T. ) ;
#7349=VERTEX_POINT ( 'NONE', #5567 ) ;
#7353=CARTESIAN_POINT ( 'NONE',  ( 217.0000000000000000, -9.000000000000001776, 18.00000000000001066 ) ) ;
#7354=ORIENTED_EDGE ( 'NONE', *, *, #406, .F. ) ;
#7361=EDGE_CURVE ( 'NONE', #734, #5579, #4987, .T. ) ;
#7364=VECTOR ( 'NONE', #5330, 1000.000000000000000 ) ;
#7365=CARTESIAN_POINT ( 'NONE',  ( 189.0478106757479395, 3.000000000000792255, 18.70974356059312527 ) ) ;
#7367=CARTESIAN_POINT ( 'NONE',  ( 187.7042711957595316, -7.845560335756932346, 15.00000000000000711 ) ) ;
#7368=SPHERICAL_SURFACE ( 'NONE', #3940, 3.000000000000000000 ) ;
#7369=CIRCLE ( 'NONE', #982, 3.000000000000000000 ) ;
#7373=CARTESIAN_POINT ( 'NONE',  ( 220.0000000000000000, -56.99999999999999289, 7.000000000000000888 ) ) ;
#7374=DIRECTION ( 'NONE',  ( 1.000000000000000000, 0.000000000000000000, 0.000000000000000000 ) ) ;
#7378=VERTEX_POINT ( 'NONE', #7332 ) ;
#7383=DIRECTION ( 'NONE',  ( -1.000000000000000000, 0.000000000000000000, 0.000000000000000000 ) ) ;
#7385=EDGE_CURVE ( 'NONE', #4834, #1345, #1983, .T. ) ;
#7391=CIRCLE ( 'NONE', #392, 3.000000000000000000 ) ;
#7397=EDGE_CURVE ( 'NONE', #1932, #5445, #6197, .T. ) ;
#7399=CARTESIAN_POINT ( 'NONE',  ( 189.5040654437683258, 3.000000000000000888, 19.50000000000000355 ) ) ;
#7401=CARTESIAN_POINT ( 'NONE',  ( 47.00000000000000000, -28.78532416918553949, 13.00000000000000711 ) ) ;
#7405=ORIENTED_EDGE ( 'NONE', *, *, #6825, .F. ) ;
#7408=DIRECTION ( 'NONE',  ( 0.000000000000000000, 1.156482317317871331E-15, -1.000000000000000000 ) ) ;
#7409=DIRECTION ( 'NONE',  ( -0.000000000000000000, -0.000000000000000000, 1.000000000000000000 ) ) ;
#7410=CYLINDRICAL_SURFACE ( 'NONE', #5957, 8.500000000000007105 ) ;
#7411=CARTESIAN_POINT ( 'NONE',  ( 47.00000000000000000, -24.98477067547739239, 35.87248741756260983 ) ) ;
#7417=EDGE_CURVE ( 'NONE', #2384, #4614, #6695, .T. ) ;
#7419=EDGE_CURVE ( 'NONE', #6206, #6714, #5351, .T. ) ;
#7421=TOROIDAL_SURFACE ( 'NONE', #3499, 7.000000000000019540, 3.000000000000000000 ) ;
#7422=CIRCLE ( 'NONE', #6325, 2.999999999999999112 ) ;
#7425=CARTESIAN_POINT ( 'NONE',  ( 49.92191802930958033, -23.56834618895300792, 12.97259539165982645 ) ) ;
#7427=CIRCLE ( 'NONE', #4360, 7.000000000000020428 ) ;
#7432=VECTOR ( 'NONE', #577, 1000.000000000000000 ) ;
#7435=PRODUCT_DEFINITION_FORMATION_WITH_SPECIFIED_SOURCE ( 'ANY', '', #3046, .NOT_KNOWN. ) ;
#7439=CARTESIAN_POINT ( 'NONE',  ( 176.5000000000000000, 39.99999999999999289, 0.000000000000000000 ) ) ;
#7440=CARTESIAN_POINT ( 'NONE',  ( 50.00000000000000000, 7.269317423140909676E-15, 13.00000000000000178 ) ) ;
#7442=ORIENTED_EDGE ( 'NONE', *, *, #1471, .F. ) ;
#7443=CARTESIAN_POINT ( 'NONE',  ( 189.5040654437683258, -3.000000000000000888, 19.50000000000000711 ) ) ;
#7444=CARTESIAN_POINT ( 'NONE',  ( 187.2596667362528535, 7.041420652221324517, 15.61258740610357876 ) ) ;
#7445=CARTESIAN_POINT ( 'NONE',  ( 220.0000000000000000, 15.08392021690038121, 12.00000000000000711 ) ) ;
#7450=ORIENTED_EDGE ( 'NONE', *, *, #103, .T. ) ;
#7451=CARTESIAN_POINT ( 'NONE',  ( 35.00000000000000000, 39.99999999999999289, 0.000000000000000000 ) ) ;
#7452=CYLINDRICAL_SURFACE ( 'NONE', #7569, 3.000000000000000000 ) ;
#7454=EDGE_CURVE ( 'NONE', #4590, #7091, #5102, .T. ) ;
#7455=DIRECTION ( 'NONE',  ( 1.000000000000000000, 0.000000000000000000, 0.000000000000000000 ) ) ;
#7460=ORIENTED_EDGE ( 'NONE', *, *, #2686, .F. ) ;
#7461=ORIENTED_EDGE ( 'NONE', *, *, #5232, .T. ) ;
#7462=CIRCLE ( 'NONE', #6846, 3.000000000000000000 ) ;
#7463=EDGE_CURVE ( 'NONE', #2786, #7465, #2644, .T. ) ;
#7465=VERTEX_POINT ( 'NONE', #6830 ) ;
#7466=CARTESIAN_POINT ( 'NONE',  ( 48.89500486289144732, -25.24885805258323757, 10.00000000000000178 ) ) ;
#7467=CARTESIAN_POINT ( 'NONE',  ( 50.04196010845020481, -18.04196010845019060, 12.50000000000000533 ) ) ;
#7468=VERTEX_POINT ( 'NONE', #1673 ) ;
#7471=EDGE_LOOP ( 'NONE', ( #5130, #1458, #5970, #2045 ) ) ;
#7473=ADVANCED_FACE ( 'NONE', ( #6336 ), #4115, .T. ) ;
#7475=CARTESIAN_POINT ( 'NONE',  ( 185.0000000000000000, -39.99999999999999289, 10.00000000000000355 ) ) ;
#7479=LINE ( 'NONE', #3373, #2150 ) ;
#7486=ORIENTED_EDGE ( 'NONE', *, *, #242, .T. ) ;
#7490=DIRECTION ( 'NONE',  ( 0.000000000000000000, 0.000000000000000000, -1.000000000000000000 ) ) ;
#7492=EDGE_LOOP ( 'NONE', ( #2247, #5326 ) ) ;
#7497=DIRECTION ( 'NONE',  ( -1.000000000000000000, 0.000000000000000000, 0.000000000000000000 ) ) ;
#7498=ORIENTED_EDGE ( 'NONE', *, *, #7521, .F. ) ;
#7503=ORIENTED_EDGE ( 'NONE', *, *, #6015, .T. ) ;
#7509=DIRECTION ( 'NONE',  ( 0.000000000000000000, 1.000000000000000000, 0.000000000000000000 ) ) ;
#7510=LINE ( 'NONE', #3290, #3980 ) ;
#7511=AXIS2_PLACEMENT_3D ( 'NONE', #821, #283, #2627 ) ;
#7516=DIRECTION ( 'NONE',  ( 0.000000000000000000, 1.000000000000000000, 0.000000000000000000 ) ) ;
#7519=FACE_OUTER_BOUND ( 'NONE', #2602, .T. ) ;
#7521=EDGE_CURVE ( 'NONE', #597, #429, #7479, .T. ) ;
#7522=ORIENTED_EDGE ( 'NONE', *, *, #1625, .F. ) ;
#7525=EDGE_CURVE ( 'NONE', #5693, #7201, #2890, .T. ) ;
#7526=CARTESIAN_POINT ( 'NONE',  ( 3.000000000000000000, 24.05453786023368323, 12.47706554351403874 ) ) ;
#7528=CARTESIAN_POINT ( 'NONE',  ( 188.6380400400057340, -8.607230116928693775, 15.00000000000001066 ) ) ;
#7529=ORIENTED_EDGE ( 'NONE', *, *, #4350, .T. ) ;
#7532=AXIS2_PLACEMENT_3D ( 'NONE', #355, #6897, #2703 ) ;
#7534=AXIS2_PLACEMENT_3D ( 'NONE', #4101, #593, #5373 ) ;
#7535=ORIENTED_EDGE ( 'NONE', *, *, #6758, .T. ) ;
#7537=LINE ( 'NONE', #5358, #7432 ) ;
#7538=VERTEX_POINT ( 'NONE', #2789 ) ;
#7544=CIRCLE ( 'NONE', #5954, 6.000000000000000000 ) ;
#7547=CARTESIAN_POINT ( 'NONE',  ( 0.000000000000000000, 21.91628335801839711, 36.91742634044857141 ) ) ;
#7548=AXIS2_PLACEMENT_3D ( 'NONE', #7353, #4473, #6892 ) ;
#7552=AXIS2_PLACEMENT_3D ( 'NONE', #7276, #5976, #3198 ) ;
#7556=EDGE_CURVE ( 'NONE', #2786, #6224, #2446, .T. ) ;
#7558=DIRECTION ( 'NONE',  ( 0.000000000000000000, 0.000000000000000000, 1.000000000000000000 ) ) ;
#7559=DIRECTION ( 'NONE',  ( 0.000000000000000000, -0.000000000000000000, 1.000000000000000000 ) ) ;
#7562=CARTESIAN_POINT ( 'NONE',  ( 188.4942707396337482, -3.000000000000000000, 17.75098426722492206 ) ) ;
#7563=PLANE ( 'NONE',  #6540 ) ;
#7569=AXIS2_PLACEMENT_3D ( 'NONE', #4039, #5765, #1716 ) ;
#7571=VERTEX_POINT ( 'NONE', #6451 ) ;
#7573=CIRCLE ( 'NONE', #2787, 8.500000000000007105 ) ;
#7576=CARTESIAN_POINT ( 'NONE',  ( 53.00000000000544986, -23.56768549070518759, 10.00000000000000888 ) ) ;
#7584=EDGE_LOOP ( 'NONE', ( #2840, #7118, #4196, #396 ) ) ;
#7586=DIRECTION ( 'NONE',  ( 0.000000000000000000, -3.304235192336777977E-16, 1.000000000000000000 ) ) ;
#7588=ORIENTED_EDGE ( 'NONE', *, *, #1839, .F. ) ;
#7590=DIRECTION ( 'NONE',  ( 1.000000000000000000, 0.000000000000000000, 0.000000000000000000 ) ) ;
#7594=CARTESIAN_POINT ( 'NONE',  ( 3.000000000000002665, 60.00000000000000000, 7.000000000000022204 ) ) ;
#7595=EDGE_CURVE ( 'NONE', #7538, #6542, #5216, .T. ) ;
#7599=CARTESIAN_POINT ( 'NONE',  ( 3.000000000000002665, -56.99999999999999289, 3.000000000000000444 ) ) ;
#7600=SPHERICAL_SURFACE ( 'NONE', #4984, 3.000000000000000000 ) ;
#7611=COLOUR_RGB('Dark Blue',0.08,0.2,0.34);
#7612=FILL_AREA_STYLE_COLOUR('',#7611);
#7613=FILL_AREA_STYLE('',(#7612));
#7614=SURFACE_STYLE_FILL_AREA(#7613);
#7615=SURFACE_SIDE_STYLE('',(#7614));
#7616=SURFACE_STYLE_USAGE(.BOTH.,#7615);
#7617=PRESENTATION_STYLE_ASSIGNMENT((#7616));
ENDSEC;
END-ISO-10303-21;
